ISO-10303-21;
HEADER;
FILE_DESCRIPTION (('STEP AP214'),
    '1' );
FILE_NAME ('hexagon nut style 1_is_IS 1364-3 - M24-W-N.step',
    '2026-10-26T19:46:16',
    ( '' ),
    ( '' ),
    'SwSTEP 2.0',
    'SolidWorks 2025',
    '' );
FILE_SCHEMA (( 'AUTOMOTIVE_DESIGN' ));
ENDSEC;

DATA;
#134=EDGE_LOOP ( 'NONE', ( #71997, #44977, #22170 ) ) ;
#225=PLANE ( 'NONE',  #9909 ) ;
#319=DIRECTION ( 'NONE',  ( -1.000000000000000000, 0.000000000000000000, -0.000000000000000000 ) ) ;
#338=VERTEX_POINT ( 'NONE', #45122 ) ;
#347=CYLINDRICAL_SURFACE ( 'NONE', #9469, 10.50000000000000000 ) ;
#382=CONICAL_SURFACE ( 'NONE', #64214, 18.00000000000000355, 1.047197551196596965 ) ;
#504=CARTESIAN_POINT ( 'NONE',  ( -18.00000000000000000, -10.39230484541329247, -1.607695154586745501 ) ) ;
#574=CARTESIAN_POINT ( 'NONE',  ( 0.000000000000000000, 0.000000000000000000, 0.000000000000000000 ) ) ;
#664=DIRECTION ( 'NONE',  ( -1.000000000000000000, 0.000000000000000000, 0.000000000000000000 ) ) ;
#728=VERTEX_POINT ( 'NONE', #11183 ) ;
#755=ORIENTED_EDGE ( 'NONE', *, *, #38449, .F. ) ;
#977=DIRECTION ( 'NONE',  ( 0.000000000000000000, 0.000000000000000000, 1.000000000000000000 ) ) ;
#990=CONICAL_SURFACE ( 'NONE', #45552, 12.00000000000000178, 0.9599310885968795892 ) ;
#1059=CARTESIAN_POINT ( 'NONE',  ( 9.000000000000023093, -15.58845726811988541, 0.000000000000000000 ) ) ;
#1378=VERTEX_POINT ( 'NONE', #55451 ) ;
#1480=VECTOR ( 'NONE', #55823, 1000.000000000000000 ) ;
#1505=VECTOR ( 'NONE', #30123, 1000.000000000000000 ) ;
#1521=CARTESIAN_POINT ( 'NONE',  ( -18.00000000000000000, -10.39230484541329425, -20.69999999999999929 ) ) ;
#1604=ORIENTED_EDGE ( 'NONE', *, *, #55621, .T. ) ;
#1666=EDGE_CURVE ( 'NONE', #64786, #22710, #45980, .T. ) ;
#1768=CARTESIAN_POINT ( 'NONE',  ( 12.00000000000000355, 0.000000000000000000, -21.50000000000000000 ) ) ;
#2034=EDGE_CURVE ( 'NONE', #35739, #24196, #65549, .T. ) ;
#2204=DIRECTION ( 'NONE',  ( 0.000000000000000000, 0.000000000000000000, 1.000000000000000000 ) ) ;
#2255=PLANE ( 'NONE',  #32383 ) ;
#2371=ORIENTED_EDGE ( 'NONE', *, *, #65856, .T. ) ;
#2444=CARTESIAN_POINT ( 'NONE',  ( 18.00000000000000000, 10.39230484541329247, -1.607695154586745501 ) ) ;
#2449=DIRECTION ( 'NONE',  ( 1.000000000000000000, 0.000000000000000000, 0.000000000000000000 ) ) ;
#2509=ORIENTED_EDGE ( 'NONE', *, *, #53355, .T. ) ;
#2671=AXIS2_PLACEMENT_3D ( 'NONE', #56861, #39129, #61769 ) ;
#2806=LINE ( 'NONE', #47698, #30288 ) ;
#2817=ORIENTED_EDGE ( 'NONE', *, *, #13618, .F. ) ;
#2891=PRODUCT_DEFINITION_SHAPE ( 'NONE', 'NONE',  #3035 ) ;
#2946=EDGE_LOOP ( 'NONE', ( #66295, #26528, #4181 ) ) ;
#2951=DIRECTION ( 'NONE',  ( -0.000000000000000000, -0.000000000000000000, 1.000000000000000000 ) ) ;
#2957=B_SPLINE_CURVE_WITH_KNOTS ( 'NONE', 3,
 ( #63274, #28579, #57266, #51219, #74604, #22534 ),
 .UNSPECIFIED., .F., .F.,
 ( 4, 2, 4 ),
 ( 2.380728323691399658E-07, 0.005257893135091114105, 0.01051554819734985997 ),
 .UNSPECIFIED. ) ;
#2960=DIRECTION ( 'NONE',  ( -0.8191520442889907994, 0.000000000000000000, -0.5735764363510474917 ) ) ;
#3035=PRODUCT_DEFINITION ( 'UNKNOWN', '', #55082, #51585 ) ;
#3283=EDGE_CURVE ( 'NONE', #38945, #71897, #33503, .T. ) ;
#3354=ORIENTED_EDGE ( 'NONE', *, *, #12254, .F. ) ;
#3417=LINE ( 'NONE', #4176, #4015 ) ;
#3552=CARTESIAN_POINT ( 'NONE',  ( -1.970469249063935269E-15, 20.78460969082654231, -20.69999999999999929 ) ) ;
#3654=CARTESIAN_POINT ( 'NONE',  ( -18.00000000000000000, -10.39230484541329425, -21.50000000000000000 ) ) ;
#3862=DIRECTION ( 'NONE',  ( 1.000000000000000000, 0.000000000000000000, 0.000000000000000000 ) ) ;
#3884=ORIENTED_EDGE ( 'NONE', *, *, #34203, .T. ) ;
#3885=VECTOR ( 'NONE', #66248, 1000.000000000000000 ) ;
#4015=VECTOR ( 'NONE', #66788, 1000.000000000000000 ) ;
#4122=CYLINDRICAL_SURFACE ( 'NONE', #20004, 18.00000000000000355 ) ;
#4167=CARTESIAN_POINT ( 'NONE',  ( -5.204170427930421283E-15, 20.78460969082654231, -1.607695154586745501 ) ) ;
#4176=CARTESIAN_POINT ( 'NONE',  ( -18.00000000000000000, 10.39230484541324628, -21.50000000000000000 ) ) ;
#4181=ORIENTED_EDGE ( 'NONE', *, *, #74544, .F. ) ;
#4207=ADVANCED_FACE ( 'NONE', ( #61059 ), #61809, .T. ) ;
#4272=DIRECTION ( 'NONE',  ( -0.000000000000000000, -0.000000000000000000, 1.000000000000000000 ) ) ;
#4541=VECTOR ( 'NONE', #55169, 999.9999999999998863 ) ;
#4563=( NAMED_UNIT ( * ) SI_UNIT ( $, .STERADIAN. ) SOLID_ANGLE_UNIT ( ) );
#4587=CARTESIAN_POINT ( 'NONE',  ( 0.000000000000000000, 0.000000000000000000, 0.000000000000000000 ) ) ;
#4614=PLANE ( 'NONE',  #40191 ) ;
#4760=CARTESIAN_POINT ( 'NONE',  ( -18.00000000000000000, -8.694318397447188929, -1.139757812215645094 ) ) ;
#4771=CARTESIAN_POINT ( 'NONE',  ( 10.91045974869143542, 14.48545281793694883, -0.07476367467994476934 ) ) ;
#4778=CARTESIAN_POINT ( 'NONE',  ( 10.53333261448113944, -14.70318727039201967, -1.996964876446738479E-14 ) ) ;
#4838=EDGE_CURVE ( 'NONE', #1378, #43896, #30248, .T. ) ;
#5072=VECTOR ( 'NONE', #39949, 999.9999999999998863 ) ;
#5194=CARTESIAN_POINT ( 'NONE',  ( -18.00000000000000000, 10.39230484541324628, -20.69999999999999929 ) ) ;
#5475=DIRECTION ( 'NONE',  ( -1.000000000000000000, 0.000000000000000000, 0.000000000000000000 ) ) ;
#5617=DIRECTION ( 'NONE',  ( -1.000000000000000000, 0.000000000000000000, 0.000000000000000000 ) ) ;
#5625=LINE ( 'NONE', #39579, #1480 ) ;
#5829=AXIS2_PLACEMENT_3D ( 'NONE', #65721, #9523, #3862 ) ;
#5957=DIRECTION ( 'NONE',  ( -0.000000000000000000, -0.000000000000000000, 1.000000000000000000 ) ) ;
#5985=ADVANCED_FACE ( 'NONE', ( #43634 ), #37443, .T. ) ;
#6031=CARTESIAN_POINT ( 'NONE',  ( -9.000000000000019540, 15.58845726811987831, -20.69999999999999929 ) ) ;
#6088=EDGE_CURVE ( 'NONE', #70161, #20252, #31999, .T. ) ;
#6291=CARTESIAN_POINT ( 'NONE',  ( -18.00000000000000000, -10.39230484541329425, -20.69999999999999929 ) ) ;
#6311=EDGE_CURVE ( 'NONE', #38945, #70823, #55592, .T. ) ;
#6321=ORIENTED_EDGE ( 'NONE', *, *, #17785, .F. ) ;
#6381=DIRECTION ( 'NONE',  ( -0.8660254037844381525, 0.5000000000000008882, 0.000000000000000000 ) ) ;
#6431=EDGE_CURVE ( 'NONE', #72356, #34530, #60702, .T. ) ;
#6493=ORIENTED_EDGE ( 'NONE', *, *, #51872, .T. ) ;
#6516=VERTEX_POINT ( 'NONE', #27305 ) ;
#6762=CARTESIAN_POINT ( 'NONE',  ( 0.000000000000000000, 0.000000000000000000, -1.050311307314560239 ) ) ;
#6815=B_SPLINE_CURVE_WITH_KNOTS ( 'NONE', 3,
 ( #70260, #34836, #17450, #47595, #40471, #58575, #18203, #23859, #52172, #504 ),
 .UNSPECIFIED., .F., .F.,
 ( 4, 2, 2, 2, 4 ),
 ( 0.01051554819734985997, 0.01182504667393350674, 0.01313454515051715524, 0.01575354210368444183, 0.02099153601001901848 ),
 .UNSPECIFIED. ) ;
#7069=DIRECTION ( 'NONE',  ( 1.000000000000000000, 0.000000000000000000, 0.000000000000000000 ) ) ;
#7096=AXIS2_PLACEMENT_3D ( 'NONE', #30856, #7486, #71206 ) ;
#7131=CARTESIAN_POINT ( 'NONE',  ( -35.99999999999995026, -2.949029909160572061E-14, 0.000000000000000000 ) ) ;
#7163=ORIENTED_EDGE ( 'NONE', *, *, #40853, .F. ) ;
#7211=LINE ( 'NONE', #29849, #30084 ) ;
#7225=VERTEX_POINT ( 'NONE', #32532 ) ;
#7360=CARTESIAN_POINT ( 'NONE',  ( 18.00000000000000000, 10.39230484541325161, -20.69999999999999929 ) ) ;
#7442=CARTESIAN_POINT ( 'NONE',  ( -7.285838599102589797E-14, -20.78460969082654231, -1.607695154586745501 ) ) ;
#7486=DIRECTION ( 'NONE',  ( -0.000000000000000000, -0.000000000000000000, -1.000000000000000000 ) ) ;
#7493=LINE ( 'NONE', #20271, #17145 ) ;
#7674=CARTESIAN_POINT ( 'NONE',  ( 12.00000000000000178, 1.469576158976824144E-15, -21.47459999999999525 ) ) ;
#7684=ORIENTED_EDGE ( 'NONE', *, *, #19767, .T. ) ;
#7756=DIRECTION ( 'NONE',  ( 0.000000000000000000, 0.000000000000000000, 1.000000000000000000 ) ) ;
#7958=EDGE_LOOP ( 'NONE', ( #72899, #29182, #47186, #34098 ) ) ;
#8051=UNCERTAINTY_MEASURE_WITH_UNIT (LENGTH_MEASURE( 1.000000000000000082E-05 ), #27935, 'distance_accuracy_value', 'NONE');
#8056=DIRECTION ( 'NONE',  ( 1.000000000000000000, 0.000000000000000000, 0.000000000000000000 ) ) ;
#8242=VERTEX_POINT ( 'NONE', #34215 ) ;
#8263=CARTESIAN_POINT ( 'NONE',  ( 7.466667385518904076, 16.47372726584778846, 2.453007415248453782E-15 ) ) ;
#8304=PRODUCT ( 'hexagon nut style 1_is_IS 1364-3 - M24-W-N', 'hexagon nut style 1_is_IS 1364-3 - M24-W-N', '', ( #11249 ) ) ;
#8551=VECTOR ( 'NONE', #23644, 1000.000000000000000 ) ;
#8768=CARTESIAN_POINT ( 'NONE',  ( 12.00000000000000000, 0.000000000000000000, 6.938893903907228378E-15 ) ) ;
#8824=DIRECTION ( 'NONE',  ( -1.000000000000000000, 0.000000000000000000, 0.000000000000000000 ) ) ;
#8896=DIRECTION ( 'NONE',  ( -1.000000000000000000, 0.000000000000000000, -0.000000000000000000 ) ) ;
#8921=CARTESIAN_POINT ( 'NONE',  ( -17.99999999999999645, -1.756128610415477631, 1.992221491942114003E-15 ) ) ;
#8958=CARTESIAN_POINT ( 'NONE',  ( 10.35000000000000142, 0.000000000000000000, -1.155342438046016218 ) ) ;
#8973=DIRECTION ( 'NONE',  ( 0.000000000000000000, 0.000000000000000000, 1.000000000000000000 ) ) ;
#8992=CARTESIAN_POINT ( 'NONE',  ( -12.00000000000000178, 0.000000000000000000, -21.47459999999999525 ) ) ;
#9017=CARTESIAN_POINT ( 'NONE',  ( 2.955318825516778158, 19.07835557137325821, -0.7126204852947338741 ) ) ;
#9030=AXIS2_PLACEMENT_3D ( 'NONE', #72572, #55978, #8824 ) ;
#9083=EDGE_LOOP ( 'NONE', ( #23389, #21966, #58924 ) ) ;
#9113=ADVANCED_FACE ( 'NONE', ( #33300, #56298 ), #4614, .F. ) ;
#9264=CARTESIAN_POINT ( 'NONE',  ( 0.000000000000000000, 0.000000000000000000, -21.47459999999999525 ) ) ;
#9267=DIRECTION ( 'NONE',  ( 1.000000000000000000, 0.000000000000000000, 0.000000000000000000 ) ) ;
#9469=AXIS2_PLACEMENT_3D ( 'NONE', #23327, #46339, #26939 ) ;
#9523=DIRECTION ( 'NONE',  ( -0.000000000000000000, -0.000000000000000000, 1.000000000000000000 ) ) ;
#9557=ORIENTED_EDGE ( 'NONE', *, *, #6088, .F. ) ;
#9660=ORIENTED_EDGE ( 'NONE', *, *, #19932, .T. ) ;
#9757=CARTESIAN_POINT ( 'NONE',  ( 0.000000000000000000, 0.000000000000000000, 6.938893903907228378E-15 ) ) ;
#9778=CARTESIAN_POINT ( 'NONE',  ( 0.000000000000000000, 0.000000000000000000, 0.000000000000000000 ) ) ;
#9909=AXIS2_PLACEMENT_3D ( 'NONE', #34176, #22447, #62817 ) ;
#9979=VECTOR ( 'NONE', #13843, 1000.000000000000000 ) ;
#10082=DIRECTION ( 'NONE',  ( -0.000000000000000000, -0.000000000000000000, 1.000000000000000000 ) ) ;
#10086=CARTESIAN_POINT ( 'NONE',  ( 0.000000000000000000, 30.78460969082653875, -20.69999999999999929 ) ) ;
#10141=CIRCLE ( 'NONE', #14918, 12.00000000000000000 ) ;
#10299=CARTESIAN_POINT ( 'NONE',  ( 0.000000000000000000, 0.000000000000000000, -20.69999999999999929 ) ) ;
#10389=DIRECTION ( 'NONE',  ( -0.000000000000000000, -0.000000000000000000, -1.000000000000000000 ) ) ;
#10762=ORIENTED_EDGE ( 'NONE', *, *, #67678, .F. ) ;
#10791=CARTESIAN_POINT ( 'NONE',  ( 9.381899668004557213, 15.36796739199404094, 2.518546589542255271E-15 ) ) ;
#10821=DIRECTION ( 'NONE',  ( -0.5000000000000012212, 0.8660254037844380415, 0.000000000000000000 ) ) ;
#11000=AXIS2_PLACEMENT_3D ( 'NONE', #18691, #47711, #36780 ) ;
#11013=B_SPLINE_CURVE_WITH_KNOTS ( 'NONE', 3,
 ( #47648, #59000, #46550, #53331, #35613, #64277, #25000, #64647, #65376, #12945 ),
 .UNSPECIFIED., .F., .F.,
 ( 4, 2, 2, 2, 4 ),
 ( 0.01051554819734978365, 0.01182504667393343735, 0.01313454515051709279, 0.01575354210368439672, 0.02099153601001901154 ),
 .UNSPECIFIED. ) ;
#11072=EDGE_LOOP ( 'NONE', ( #74566, #73098, #39123, #21897, #24947, #35764 ) ) ;
#11139=CIRCLE ( 'NONE', #2671, 10.50000000000000000 ) ;
#11183=CARTESIAN_POINT ( 'NONE',  ( 18.00000000000000355, 0.000000000000000000, -21.50000000000000000 ) ) ;
#11198=EDGE_CURVE ( 'NONE', #24196, #17730, #10141, .T. ) ;
#11249=PRODUCT_CONTEXT ( 'NONE', #14382, 'mechanical' ) ;
#11350=ADVANCED_FACE ( 'NONE', ( #12350 ), #69701, .T. ) ;
#11414=CONICAL_SURFACE ( 'NONE', #74091, 18.00000000000000355, 1.047197551196596965 ) ;
#11422=DIRECTION ( 'NONE',  ( 0.000000000000000000, 0.000000000000000000, 1.000000000000000000 ) ) ;
#11448=EDGE_CURVE ( 'NONE', #39015, #6516, #64772, .T. ) ;
#11481=DIRECTION ( 'NONE',  ( 1.000000000000000000, 0.000000000000000000, 0.000000000000000000 ) ) ;
#11516=ADVANCED_FACE ( 'NONE', ( #36110 ), #59128, .T. ) ;
#11608=CARTESIAN_POINT ( 'NONE',  ( 18.00000000000000000, 10.39230484541325161, -20.69999999999999929 ) ) ;
#11636=VECTOR ( 'NONE', #2960, 1000.000000000000114 ) ;
#11842=EDGE_CURVE ( 'NONE', #72356, #20252, #51124, .T. ) ;
#11907=DIRECTION ( 'NONE',  ( 0.000000000000000000, -1.000000000000000000, 0.000000000000000000 ) ) ;
#11994=ADVANCED_BREP_SHAPE_REPRESENTATION ( '', ( #65418, #57354 ), #17638 ) ;
#12035=DIRECTION ( 'NONE',  ( 1.000000000000000000, 0.000000000000000000, 0.000000000000000000 ) ) ;
#12254=EDGE_CURVE ( 'NONE', #6516, #338, #64330, .T. ) ;
#12350=FACE_OUTER_BOUND ( 'NONE', #11072, .T. ) ;
#12357=AXIS2_PLACEMENT_3D ( 'NONE', #61409, #37286, #71966 ) ;
#12485=DIRECTION ( 'NONE',  ( 0.000000000000000000, -1.000000000000000000, 0.000000000000000000 ) ) ;
#12575=ORIENTED_EDGE ( 'NONE', *, *, #49584, .T. ) ;
#12610=ORIENTED_EDGE ( 'NONE', *, *, #16376, .T. ) ;
#12709=ORIENTED_EDGE ( 'NONE', *, *, #61700, .F. ) ;
#12945=CARTESIAN_POINT ( 'NONE',  ( -5.204170427930421283E-15, 20.78460969082654231, -1.607695154586745501 ) ) ;
#13111=CARTESIAN_POINT ( 'NONE',  ( 9.000000000000023093, -15.58845726811988541, 0.000000000000000000 ) ) ;
#13328=CARTESIAN_POINT ( 'NONE',  ( 0.000000000000000000, 0.000000000000000000, 6.938893903907228378E-15 ) ) ;
#13334=ORIENTED_EDGE ( 'NONE', *, *, #50919, .T. ) ;
#13444=CARTESIAN_POINT ( 'NONE',  ( 5.951239500248227898, -17.34865996334632143, -0.1850551574587783465 ) ) ;
#13455=DIRECTION ( 'NONE',  ( 0.000000000000000000, 0.000000000000000000, -1.000000000000000000 ) ) ;
#13534=CARTESIAN_POINT ( 'NONE',  ( 5.952395412842803601, 17.34799259689864570, -0.1532218116813576225 ) ) ;
#13618=EDGE_CURVE ( 'NONE', #51583, #37575, #62821, .T. ) ;
#13843=DIRECTION ( 'NONE',  ( 0.8191520442889911324, 0.000000000000000000, 0.5735764363510471586 ) ) ;
#14140=DIRECTION ( 'NONE',  ( -1.000000000000000000, 0.000000000000000000, 0.000000000000000000 ) ) ;
#14164=FACE_OUTER_BOUND ( 'NONE', #70890, .T. ) ;
#14195=DIRECTION ( 'NONE',  ( -1.000000000000000000, 0.000000000000000000, 0.000000000000000000 ) ) ;
#14237=AXIS2_PLACEMENT_3D ( 'NONE', #63314, #57306, #5617 ) ;
#14258=LINE ( 'NONE', #8992, #11636 ) ;
#14265=EDGE_CURVE ( 'NONE', #728, #26967, #30312, .T. ) ;
#14382=APPLICATION_CONTEXT ( 'automotive_design' ) ;
#14412=EDGE_CURVE ( 'NONE', #338, #70161, #16351, .T. ) ;
#14538=ADVANCED_FACE ( 'NONE', ( #25631 ), #63510, .F. ) ;
#14643=CARTESIAN_POINT ( 'NONE',  ( 0.000000000000000000, 0.000000000000000000, -21.50000000000000000 ) ) ;
#14715=ORIENTED_EDGE ( 'NONE', *, *, #20387, .T. ) ;
#14918=AXIS2_PLACEMENT_3D ( 'NONE', #9757, #21430, #44823 ) ;
#14925=LINE ( 'NONE', #19850, #3885 ) ;
#15137=SHAPE_REPRESENTATION ( 'hexagon nut style 1_is_IS 1364-3 - M24-W-N', ( #57354 ), #17638 ) ;
#15259=ORIENTED_EDGE ( 'NONE', *, *, #45905, .F. ) ;
#15296=ORIENTED_EDGE ( 'NONE', *, *, #3283, .T. ) ;
#15306=CARTESIAN_POINT ( 'NONE',  ( -18.00000000000000355, 0.000000000000000000, 0.000000000000000000 ) ) ;
#15366=EDGE_LOOP ( 'NONE', ( #45752, #39600, #44890 ) ) ;
#15656=CARTESIAN_POINT ( 'NONE',  ( 0.000000000000000000, 0.000000000000000000, 0.000000000000000000 ) ) ;
#15938=PLANE ( 'NONE',  #65243 ) ;
#16003=DIRECTION ( 'NONE',  ( -0.000000000000000000, -0.000000000000000000, 1.000000000000000000 ) ) ;
#16005=VECTOR ( 'NONE', #31156, 1000.000000000000000 ) ;
#16089=CARTESIAN_POINT ( 'NONE',  ( -1.970469249063935269E-15, 20.78460969082654231, -21.50000000000000000 ) ) ;
#16172=CARTESIAN_POINT ( 'NONE',  ( 18.00000000000000000, 10.39230484541325161, -21.50000000000000000 ) ) ;
#16182=CIRCLE ( 'NONE', #65578, 12.00000000000000355 ) ;
#16260=ORIENTED_EDGE ( 'NONE', *, *, #68183, .T. ) ;
#16302=DIRECTION ( 'NONE',  ( 0.8660254037844379305, 0.5000000000000011102, 0.000000000000000000 ) ) ;
#16351=LINE ( 'NONE', #51075, #35016 ) ;
#16359=ORIENTED_EDGE ( 'NONE', *, *, #17785, .T. ) ;
#16376=EDGE_CURVE ( 'NONE', #728, #6516, #51456, .T. ) ;
#16399=EDGE_CURVE ( 'NONE', #7225, #338, #56386, .T. ) ;
#16676=DIRECTION ( 'NONE',  ( 0.5000000000000012212, -0.8660254037844380415, 0.000000000000000000 ) ) ;
#16743=DIRECTION ( 'NONE',  ( -0.000000000000000000, -0.000000000000000000, 1.000000000000000000 ) ) ;
#16893=SHAPE_DEFINITION_REPRESENTATION ( #2891, #15137 ) ;
#16925=LINE ( 'NONE', #62574, #5072 ) ;
#16980=CARTESIAN_POINT ( 'NONE',  ( 9.000000000000014211, 15.58845726811988541, -20.69999999999999929 ) ) ;
#17048=DIRECTION ( 'NONE',  ( -0.000000000000000000, -0.000000000000000000, -1.000000000000000000 ) ) ;
#17060=DIRECTION ( 'NONE',  ( 1.000000000000000000, 0.000000000000000000, 0.000000000000000000 ) ) ;
#17062=CIRCLE ( 'NONE', #32763, 18.00000000000000355 ) ;
#17105=CARTESIAN_POINT ( 'NONE',  ( -18.00000000000000000, 1.759986210487456626, -0.03733711119006485196 ) ) ;
#17112=CIRCLE ( 'NONE', #67748, 12.00000000000000178 ) ;
#17125=CARTESIAN_POINT ( 'NONE',  ( 18.00000000000000355, 0.000000000000000000, 0.000000000000000000 ) ) ;
#17145=VECTOR ( 'NONE', #8973, 1000.000000000000000 ) ;
#17195=AXIS2_PLACEMENT_3D ( 'NONE', #46093, #17048, #44986 ) ;
#17354=( LENGTH_UNIT ( ) NAMED_UNIT ( * ) SI_UNIT ( .MILLI., .METRE. ) );
#17450=CARTESIAN_POINT ( 'NONE',  ( -9.765709903158434457, -15.14637444941025635, -0.009429105422181003823 ) ) ;
#17638=( GEOMETRIC_REPRESENTATION_CONTEXT ( 3 ) GLOBAL_UNCERTAINTY_ASSIGNED_CONTEXT ( ( #29804 ) ) GLOBAL_UNIT_ASSIGNED_CONTEXT ( ( #17354, #69417, #4563 ) ) REPRESENTATION_CONTEXT ( 'NONE', 'WORKASPACE' ) );
#17662=AXIS2_PLACEMENT_3D ( 'NONE', #72735, #2951, #19543 ) ;
#17729=ORIENTED_EDGE ( 'NONE', *, *, #11842, .F. ) ;
#17730=VERTEX_POINT ( 'NONE', #59462 ) ;
#17785=EDGE_CURVE ( 'NONE', #20313, #35739, #41371, .T. ) ;
#17941=CARTESIAN_POINT ( 'NONE',  ( 9.000000000000014211, 15.58845726811988719, 0.000000000000000000 ) ) ;
#17987=ORIENTED_EDGE ( 'NONE', *, *, #48541, .T. ) ;
#18011=LINE ( 'NONE', #45933, #50009 ) ;
#18052=DIRECTION ( 'NONE',  ( -0.000000000000000000, -0.000000000000000000, 1.000000000000000000 ) ) ;
#18115=DIRECTION ( 'NONE',  ( 1.000000000000000000, 0.000000000000000000, 0.000000000000000000 ) ) ;
#18142=AXIS2_PLACEMENT_3D ( 'NONE', #25904, #54609, #72699 ) ;
#18159=ORIENTED_EDGE ( 'NONE', *, *, #4838, .T. ) ;
#18203=CARTESIAN_POINT ( 'NONE',  ( -12.80255146922223375, -13.39305315375707295, -0.2939692054342312177 ) ) ;
#18218=DIRECTION ( 'NONE',  ( 0.000000000000000000, 0.000000000000000000, 1.000000000000000000 ) ) ;
#18450=CIRCLE ( 'NONE', #53399, 18.00000000000000000 ) ;
#18691=CARTESIAN_POINT ( 'NONE',  ( 0.000000000000000000, 0.000000000000000000, -20.69999999999999929 ) ) ;
#18729=ADVANCED_FACE ( 'NONE', ( #62706 ), #15938, .T. ) ;
#18768=EDGE_CURVE ( 'NONE', #6516, #64786, #17062, .T. ) ;
#18868=DIRECTION ( 'NONE',  ( 0.000000000000000000, 0.000000000000000000, 1.000000000000000000 ) ) ;
#19023=VERTEX_POINT ( 'NONE', #17941 ) ;
#19050=CARTESIAN_POINT ( 'NONE',  ( 18.00000000000000000, 4.406054334071555445, -0.2960025734007551979 ) ) ;
#19052=CONICAL_SURFACE ( 'NONE', #5829, 10.35000000000000142, 0.9599310885968800333 ) ;
#19193=CIRCLE ( 'NONE', #28850, 10.50000000000000000 ) ;
#19200=DIRECTION ( 'NONE',  ( -0.000000000000000000, -0.000000000000000000, -1.000000000000000000 ) ) ;
#19228=DIRECTION ( 'NONE',  ( 0.000000000000000000, 0.000000000000000000, -1.000000000000000000 ) ) ;
#19340=ORIENTED_EDGE ( 'NONE', *, *, #21299, .F. ) ;
#19543=DIRECTION ( 'NONE',  ( 1.000000000000000000, 0.000000000000000000, 0.000000000000000000 ) ) ;
#19605=AXIS2_PLACEMENT_3D ( 'NONE', #13328, #65763, #8056 ) ;
#19767=EDGE_CURVE ( 'NONE', #22710, #62930, #5625, .T. ) ;
#19850=CARTESIAN_POINT ( 'NONE',  ( -10.35000000000000142, 1.267509437117510795E-15, -1.155342438046016218 ) ) ;
#19873=FACE_OUTER_BOUND ( 'NONE', #64204, .T. ) ;
#19889=CARTESIAN_POINT ( 'NONE',  ( 0.000000000000000000, 0.000000000000000000, 0.000000000000000000 ) ) ;
#19932=EDGE_CURVE ( 'NONE', #38109, #51876, #16925, .T. ) ;
#20004=AXIS2_PLACEMENT_3D ( 'NONE', #9778, #48997, #61823 ) ;
#20050=EDGE_CURVE ( 'NONE', #33535, #31504, #17112, .T. ) ;
#20061=FACE_OUTER_BOUND ( 'NONE', #7958, .T. ) ;
#20096=ORIENTED_EDGE ( 'NONE', *, *, #16399, .T. ) ;
#20194=DIRECTION ( 'NONE',  ( 0.000000000000000000, 0.000000000000000000, -1.000000000000000000 ) ) ;
#20211=ORIENTED_EDGE ( 'NONE', *, *, #44227, .T. ) ;
#20252=VERTEX_POINT ( 'NONE', #13111 ) ;
#20271=CARTESIAN_POINT ( 'NONE',  ( 18.00000000000000000, 10.39230484541325161, -21.50000000000000000 ) ) ;
#20313=VERTEX_POINT ( 'NONE', #71196 ) ;
#20371=EDGE_CURVE ( 'NONE', #37575, #33535, #59527, .T. ) ;
#20387=EDGE_CURVE ( 'NONE', #64105, #17730, #14925, .T. ) ;
#20416=EDGE_LOOP ( 'NONE', ( #43817, #14715, #22505, #33849 ) ) ;
#20542=ADVANCED_FACE ( 'NONE', ( #67753 ), #225, .T. ) ;
#20640=CIRCLE ( 'NONE', #62807, 10.50000000000000000 ) ;
#20779=CARTESIAN_POINT ( 'NONE',  ( -18.00000000000000000, 0.000000000000000000, -20.69999999999999929 ) ) ;
#21012=AXIS2_PLACEMENT_3D ( 'NONE', #38337, #27746, #62084 ) ;
#21299=EDGE_CURVE ( 'NONE', #41754, #1378, #6815, .T. ) ;
#21392=DIRECTION ( 'NONE',  ( -1.000000000000000000, 0.000000000000000000, -0.000000000000000000 ) ) ;
#21430=DIRECTION ( 'NONE',  ( -0.000000000000000000, -0.000000000000000000, 1.000000000000000000 ) ) ;
#21880=CIRCLE ( 'NONE', #50805, 18.00000000000000355 ) ;
#21897=ORIENTED_EDGE ( 'NONE', *, *, #71726, .F. ) ;
#21966=ORIENTED_EDGE ( 'NONE', *, *, #6431, .T. ) ;
#22127=DIRECTION ( 'NONE',  ( 1.000000000000000000, 0.000000000000000000, 0.000000000000000000 ) ) ;
#22149=AXIS2_PLACEMENT_3D ( 'NONE', #30447, #28960, #319 ) ;
#22170=ORIENTED_EDGE ( 'NONE', *, *, #30518, .F. ) ;
#22191=AXIS2_PLACEMENT_3D ( 'NONE', #58758, #5957, #7069 ) ;
#22224=( GEOMETRIC_REPRESENTATION_CONTEXT ( 3 ) GLOBAL_UNCERTAINTY_ASSIGNED_CONTEXT ( ( #8051 ) ) GLOBAL_UNIT_ASSIGNED_CONTEXT ( ( #27935, #68666, #50199 ) ) REPRESENTATION_CONTEXT ( 'NONE', 'WORKASPACE' ) );
#22258=AXIS2_PLACEMENT_3D ( 'NONE', #16089, #10821, #74189 ) ;
#22333=CARTESIAN_POINT ( 'NONE',  ( -18.00000000000000355, 2.204364238465235822E-15, -21.50000000000000000 ) ) ;
#22342=ORIENTED_EDGE ( 'NONE', *, *, #20050, .T. ) ;
#22377=CARTESIAN_POINT ( 'NONE',  ( 18.00000000000000355, -10.39230484541328892, -1.607695154586745501 ) ) ;
#22396=ORIENTED_EDGE ( 'NONE', *, *, #52993, .F. ) ;
#22447=DIRECTION ( 'NONE',  ( 0.000000000000000000, 0.000000000000000000, -1.000000000000000000 ) ) ;
#22498=CARTESIAN_POINT ( 'NONE',  ( 18.00000000000000000, -6.103439543526004485, -0.5706341627281751316 ) ) ;
#22505=ORIENTED_EDGE ( 'NONE', *, *, #52267, .T. ) ;
#22534=CARTESIAN_POINT ( 'NONE',  ( -9.000000000000017764, -15.58845726811988719, 0.000000000000000000 ) ) ;
#22555=ADVANCED_FACE ( 'NONE', ( #24686 ), #41686, .T. ) ;
#22710=VERTEX_POINT ( 'NONE', #3552 ) ;
#23327=CARTESIAN_POINT ( 'NONE',  ( 0.000000000000000000, 0.000000000000000000, -21.50000000000000000 ) ) ;
#23389=ORIENTED_EDGE ( 'NONE', *, *, #47816, .F. ) ;
#23415=FACE_OUTER_BOUND ( 'NONE', #72121, .T. ) ;
#23473=EDGE_LOOP ( 'NONE', ( #58279, #28950, #34578 ) ) ;
#23565=CONICAL_SURFACE ( 'NONE', #44047, 18.00000000000000355, 1.047197551196596965 ) ;
#23566=EDGE_CURVE ( 'NONE', #43896, #39105, #33433, .T. ) ;
#23644=DIRECTION ( 'NONE',  ( 0.000000000000000000, 0.000000000000000000, 1.000000000000000000 ) ) ;
#23732=CARTESIAN_POINT ( 'NONE',  ( -12.00000000000000178, 0.000000000000000000, -21.47459999999999525 ) ) ;
#23787=FACE_OUTER_BOUND ( 'NONE', #50807, .T. ) ;
#23859=CARTESIAN_POINT ( 'NONE',  ( -15.05053643744965264, -12.09517842721673553, -0.7140392532422581429 ) ) ;
#23897=LINE ( 'NONE', #51829, #26466 ) ;
#24126=VERTEX_POINT ( 'NONE', #49115 ) ;
#24196=VERTEX_POINT ( 'NONE', #8768 ) ;
#24340=CARTESIAN_POINT ( 'NONE',  ( 18.00000000000000000, 1.759986210487464176, -0.03733711119006424134 ) ) ;
#24386=CARTESIAN_POINT ( 'NONE',  ( 0.000000000000000000, 0.000000000000000000, -20.69999999999999929 ) ) ;
#24522=CYLINDRICAL_SURFACE ( 'NONE', #66227, 10.50000000000000000 ) ;
#24686=FACE_OUTER_BOUND ( 'NONE', #27387, .T. ) ;
#24947=ORIENTED_EDGE ( 'NONE', *, *, #18768, .F. ) ;
#25000=CARTESIAN_POINT ( 'NONE',  ( -5.197448530777805331, 17.78386138248274051, -0.2939692054342110672 ) ) ;
#25062=CARTESIAN_POINT ( 'NONE',  ( 17.99999999999999645, 8.711927089654787792, -1.122611879773029120 ) ) ;
#25398=CARTESIAN_POINT ( 'NONE',  ( -10.50000000000000000, 1.285879139104720831E-15, -1.050311307314560239 ) ) ;
#25453=ORIENTED_EDGE ( 'NONE', *, *, #47816, .T. ) ;
#25529=VECTOR ( 'NONE', #7756, 1000.000000000000000 ) ;
#25569=DIRECTION ( 'NONE',  ( 1.000000000000000000, 0.000000000000000000, -0.000000000000000000 ) ) ;
#25631=FACE_OUTER_BOUND ( 'NONE', #62722, .T. ) ;
#25852=CARTESIAN_POINT ( 'NONE',  ( 0.000000000000000000, 30.78460969082653875, -20.69999999999999929 ) ) ;
#25904=CARTESIAN_POINT ( 'NONE',  ( 0.000000000000000000, 0.000000000000000000, -20.69999999999999929 ) ) ;
#25935=ORIENTED_EDGE ( 'NONE', *, *, #68183, .F. ) ;
#26466=VECTOR ( 'NONE', #51449, 1000.000000000000114 ) ;
#26528=ORIENTED_EDGE ( 'NONE', *, *, #6311, .T. ) ;
#26629=VECTOR ( 'NONE', #50711, 1000.000000000000114 ) ;
#26679=CARTESIAN_POINT ( 'NONE',  ( 18.00000000000000355, -10.39230484541328892, -1.607695154586745501 ) ) ;
#26939=DIRECTION ( 'NONE',  ( 1.000000000000000000, 0.000000000000000000, 0.000000000000000000 ) ) ;
#26967=VERTEX_POINT ( 'NONE', #22333 ) ;
#27054=FACE_OUTER_BOUND ( 'NONE', #73257, .T. ) ;
#27058=CARTESIAN_POINT ( 'NONE',  ( 18.00000000000000000, -8.694318397447183600, -1.139757812215642430 ) ) ;
#27116=CONICAL_SURFACE ( 'NONE', #48805, 10.35000000000000142, 0.9599310885968800333 ) ;
#27305=CARTESIAN_POINT ( 'NONE',  ( 18.00000000000000000, 0.000000000000000000, -20.69999999999999929 ) ) ;
#27387=EDGE_LOOP ( 'NONE', ( #20211, #18159, #43321, #57129, #35472, #15296 ) ) ;
#27394=CARTESIAN_POINT ( 'NONE',  ( 12.04760458715722748, -13.82892193934116776, -0.1532218116813789111 ) ) ;
#27399=CARTESIAN_POINT ( 'NONE',  ( 0.000000000000000000, 0.000000000000000000, -21.50000000000000000 ) ) ;
#27441=ORIENTED_EDGE ( 'NONE', *, *, #12254, .T. ) ;
#27611=CARTESIAN_POINT ( 'NONE',  ( -35.99999999999995026, -2.949029909160572061E-14, -21.50000000000000000 ) ) ;
#27700=CARTESIAN_POINT ( 'NONE',  ( 1.502314598737163567E-15, -20.78460969082658494, -20.69999999999999929 ) ) ;
#27746=DIRECTION ( 'NONE',  ( -0.000000000000000000, -0.000000000000000000, -1.000000000000000000 ) ) ;
#27763=CARTESIAN_POINT ( 'NONE',  ( 16.53139458858881738, 11.24020457502483872, -1.118160017449573385 ) ) ;
#27935=( LENGTH_UNIT ( ) NAMED_UNIT ( * ) SI_UNIT ( .MILLI., .METRE. ) );
#28017=VECTOR ( 'NONE', #51571, 1000.000000000000000 ) ;
#28062=CARTESIAN_POINT ( 'NONE',  ( -18.00000000000000355, 7.009507535100746978, -0.7186345456308798063 ) ) ;
#28076=AXIS2_PLACEMENT_3D ( 'NONE', #25852, #20194, #8896 ) ;
#28173=CARTESIAN_POINT ( 'NONE',  ( 18.00000000000000000, -6.968949133139053842, -0.7423331077269011979 ) ) ;
#28232=CARTESIAN_POINT ( 'NONE',  ( -15.04468117448323028, 12.09855896486652505, -0.7126204852947278789 ) ) ;
#28579=CARTESIAN_POINT ( 'NONE',  ( -1.472282454178774014, -19.93458701958330082, -1.116934336526977711 ) ) ;
#28603=CARTESIAN_POINT ( 'NONE',  ( -12.04760458715721505, 13.82892193934112690, -0.1532218116813564290 ) ) ;
#28671=ORIENTED_EDGE ( 'NONE', *, *, #23566, .F. ) ;
#28804=CARTESIAN_POINT ( 'NONE',  ( -18.00000000000000355, 0.000000000000000000, 0.000000000000000000 ) ) ;
#28850=AXIS2_PLACEMENT_3D ( 'NONE', #73671, #45366, #44633 ) ;
#28938=FACE_OUTER_BOUND ( 'NONE', #61624, .T. ) ;
#28950=ORIENTED_EDGE ( 'NONE', *, *, #18768, .T. ) ;
#28960=DIRECTION ( 'NONE',  ( 0.000000000000000000, 0.000000000000000000, -1.000000000000000000 ) ) ;
#28972=B_SPLINE_CURVE_WITH_KNOTS ( 'NONE', 3,
 ( #63672, #57291, #28232, #28603, #52367, #64054 ),
 .UNSPECIFIED., .F., .F.,
 ( 4, 2, 4 ),
 ( 2.380728322768173715E-07, 0.005257893135091030838, 0.01051554819734978365 ),
 .UNSPECIFIED. ) ;
#29182=ORIENTED_EDGE ( 'NONE', *, *, #45905, .T. ) ;
#29318=DIRECTION ( 'NONE',  ( 0.000000000000000000, 0.000000000000000000, -1.000000000000000000 ) ) ;
#29801=ADVANCED_FACE ( 'NONE', ( #23415 ), #24522, .F. ) ;
#29804=UNCERTAINTY_MEASURE_WITH_UNIT (LENGTH_MEASURE( 1.000000000000000082E-05 ), #17354, 'distance_accuracy_value', 'NONE');
#29849=CARTESIAN_POINT ( 'NONE',  ( -18.00000000000000000, 10.39230484541324628, -20.69999999999999929 ) ) ;
#30084=VECTOR ( 'NONE', #12485, 1000.000000000000000 ) ;
#30123=DIRECTION ( 'NONE',  ( 0.000000000000000000, 0.000000000000000000, 1.000000000000000000 ) ) ;
#30248=B_SPLINE_CURVE_WITH_KNOTS ( 'NONE', 3,
 ( #39085, #73411, #4760, #43615, #62090, #49655, #8921, #15306 ),
 .UNSPECIFIED., .F., .F.,
 ( 4, 2, 2, 4 ),
 ( 0.01854123755286043312, 0.02116956588062352679, 0.02379789420838662392, 0.02905455086391281472 ),
 .UNSPECIFIED. ) ;
#30288=VECTOR ( 'NONE', #70719, 1000.000000000000000 ) ;
#30312=CIRCLE ( 'NONE', #72470, 18.00000000000000355 ) ;
#30378=CARTESIAN_POINT ( 'NONE',  ( 18.00000000000000355, 0.8785859941773086490, 1.951563910473907981E-15 ) ) ;
#30379=ORIENTED_EDGE ( 'NONE', *, *, #67678, .T. ) ;
#30394=LINE ( 'NONE', #60167, #25529 ) ;
#30447=CARTESIAN_POINT ( 'NONE',  ( 0.000000000000000000, 30.78460969082653875, -20.69999999999999929 ) ) ;
#30448=AXIS2_PLACEMENT_3D ( 'NONE', #36720, #31425, #70315 ) ;
#30483=DIRECTION ( 'NONE',  ( -0.000000000000000000, -0.000000000000000000, 1.000000000000000000 ) ) ;
#30507=PLANE ( 'NONE',  #60556 ) ;
#30518=EDGE_CURVE ( 'NONE', #24126, #7225, #23897, .T. ) ;
#30539=ORIENTED_EDGE ( 'NONE', *, *, #65856, .F. ) ;
#30730=CARTESIAN_POINT ( 'NONE',  ( -18.00000000000000000, 10.39230484541324628, -21.50000000000000000 ) ) ;
#30856=CARTESIAN_POINT ( 'NONE',  ( 0.000000000000000000, 0.000000000000000000, 0.000000000000000000 ) ) ;
#31043=EDGE_CURVE ( 'NONE', #70823, #7225, #43388, .T. ) ;
#31156=DIRECTION ( 'NONE',  ( -0.000000000000000000, -0.000000000000000000, 1.000000000000000000 ) ) ;
#31244=DIRECTION ( 'NONE',  ( 0.000000000000000000, 0.000000000000000000, -1.000000000000000000 ) ) ;
#31425=DIRECTION ( 'NONE',  ( 0.000000000000000000, 0.000000000000000000, -1.000000000000000000 ) ) ;
#31504=VERTEX_POINT ( 'NONE', #7674 ) ;
#31536=PLANE ( 'NONE',  #28076 ) ;
#31548=EDGE_CURVE ( 'NONE', #39105, #62930, #11013, .T. ) ;
#31579=DIRECTION ( 'NONE',  ( 0.8660254037844380415, -0.5000000000000009992, 0.000000000000000000 ) ) ;
#31772=EDGE_LOOP ( 'NONE', ( #17729, #25453, #72027, #28671, #56094, #37930 ) ) ;
#31844=ORIENTED_EDGE ( 'NONE', *, *, #53630, .T. ) ;
#31952=PLANE ( 'NONE',  #50454 ) ;
#31999=B_SPLINE_CURVE_WITH_KNOTS ( 'NONE', 3,
 ( #33096, #55347, #73428, #27394, #4778, #62107 ),
 .UNSPECIFIED., .F., .F.,
 ( 4, 2, 4 ),
 ( 2.380728322738124163E-07, 0.005257893135091018695, 0.01051554819734976456 ),
 .UNSPECIFIED. ) ;
#32360=CARTESIAN_POINT ( 'NONE',  ( 18.00000000000000355, -9.547192751170710423, -1.363732307033565405 ) ) ;
#32383=AXIS2_PLACEMENT_3D ( 'NONE', #70914, #19228, #46791 ) ;
#32480=ADVANCED_FACE ( 'NONE', ( #37945 ), #990, .F. ) ;
#32532=CARTESIAN_POINT ( 'NONE',  ( 9.000000000000040856, -15.58845726811991739, -20.69999999999999929 ) ) ;
#32655=ORIENTED_EDGE ( 'NONE', *, *, #52267, .F. ) ;
#32687=ORIENTED_EDGE ( 'NONE', *, *, #14412, .F. ) ;
#32763=AXIS2_PLACEMENT_3D ( 'NONE', #10299, #4272, #17060 ) ;
#32966=ADVANCED_FACE ( 'NONE', ( #20061 ), #19052, .F. ) ;
#33049=DIRECTION ( 'NONE',  ( 0.000000000000000000, 0.000000000000000000, -1.000000000000000000 ) ) ;
#33096=CARTESIAN_POINT ( 'NONE',  ( 18.00000000000000355, -10.39230484541328892, -1.607695154586745501 ) ) ;
#33166=ORIENTED_EDGE ( 'NONE', *, *, #71458, .F. ) ;
#33300=FACE_BOUND ( 'NONE', #48676, .T. ) ;
#33433=CIRCLE ( 'NONE', #55129, 18.00000000000000000 ) ;
#33453=CARTESIAN_POINT ( 'NONE',  ( 9.765709903158406036, 15.14637444941022792, -0.009429105422156979638 ) ) ;
#33503=LINE ( 'NONE', #5194, #28017 ) ;
#33535=VERTEX_POINT ( 'NONE', #23732 ) ;
#33570=CIRCLE ( 'NONE', #56435, 18.00000000000000355 ) ;
#33849=ORIENTED_EDGE ( 'NONE', *, *, #2034, .F. ) ;
#34089=DIRECTION ( 'NONE',  ( 0.8660254037844380415, -0.5000000000000009992, 0.000000000000000000 ) ) ;
#34098=ORIENTED_EDGE ( 'NONE', *, *, #11198, .T. ) ;
#34176=CARTESIAN_POINT ( 'NONE',  ( 0.000000000000000000, 30.78460969082653875, -20.69999999999999929 ) ) ;
#34203=EDGE_CURVE ( 'NONE', #38109, #38945, #33570, .T. ) ;
#34215=CARTESIAN_POINT ( 'NONE',  ( -7.285838599102589797E-14, -20.78460969082654231, -1.607695154586745501 ) ) ;
#34362=ORIENTED_EDGE ( 'NONE', *, *, #14265, .T. ) ;
#34459=DIRECTION ( 'NONE',  ( 1.000000000000000000, 0.000000000000000000, 0.000000000000000000 ) ) ;
#34530=VERTEX_POINT ( 'NONE', #47516 ) ;
#34578=ORIENTED_EDGE ( 'NONE', *, *, #46299, .F. ) ;
#34836=CARTESIAN_POINT ( 'NONE',  ( -9.381899668004583859, -15.36796739199406225, -2.007213975108514882E-14 ) ) ;
#35016=VECTOR ( 'NONE', #69174, 1000.000000000000000 ) ;
#35066=CIRCLE ( 'NONE', #48259, 18.00000000000000355 ) ;
#35083=ORIENTED_EDGE ( 'NONE', *, *, #20371, .T. ) ;
#35090=EDGE_LOOP ( 'NONE', ( #25935, #59408, #56340, #68364 ) ) ;
#35105=EDGE_LOOP ( 'NONE', ( #12709, #32687, #3354, #35826, #12575, #48974 ) ) ;
#35306=ADVANCED_FACE ( 'NONE', ( #19873 ), #31952, .T. ) ;
#35472=ORIENTED_EDGE ( 'NONE', *, *, #55381, .T. ) ;
#35594=CARTESIAN_POINT ( 'NONE',  ( -18.00000000000000000, 10.39230484541324628, -1.607695154586745501 ) ) ;
#35613=CARTESIAN_POINT ( 'NONE',  ( -7.089540251308589447, 16.69146171830283265, -0.07476367467994493587 ) ) ;
#35664=DIRECTION ( 'NONE',  ( -1.000000000000000000, 0.000000000000000000, 0.000000000000000000 ) ) ;
#35732=ORIENTED_EDGE ( 'NONE', *, *, #45005, .F. ) ;
#35739=VERTEX_POINT ( 'NONE', #64366 ) ;
#35764=ORIENTED_EDGE ( 'NONE', *, *, #16376, .F. ) ;
#35826=ORIENTED_EDGE ( 'NONE', *, *, #11448, .F. ) ;
#36110=FACE_OUTER_BOUND ( 'NONE', #134, .T. ) ;
#36256=FACE_OUTER_BOUND ( 'NONE', #20416, .T. ) ;
#36492=CARTESIAN_POINT ( 'NONE',  ( 0.000000000000000000, 0.000000000000000000, 0.000000000000000000 ) ) ;
#36499=ORIENTED_EDGE ( 'NONE', *, *, #20050, .F. ) ;
#36519=ORIENTED_EDGE ( 'NONE', *, *, #11198, .F. ) ;
#36720=CARTESIAN_POINT ( 'NONE',  ( 0.000000000000000000, 30.78460969082653875, -20.69999999999999929 ) ) ;
#36780=DIRECTION ( 'NONE',  ( 1.000000000000000000, 0.000000000000000000, 0.000000000000000000 ) ) ;
#36851=CARTESIAN_POINT ( 'NONE',  ( 2.949463562550349138, -19.08173610902314721, -0.7140392532422756844 ) ) ;
#36893=CARTESIAN_POINT ( 'NONE',  ( -18.00000000000000000, -10.39230484541329425, -21.50000000000000000 ) ) ;
#37098=ORIENTED_EDGE ( 'NONE', *, *, #43890, .F. ) ;
#37213=LINE ( 'NONE', #67652, #65773 ) ;
#37286=DIRECTION ( 'NONE',  ( 0.000000000000000000, 0.000000000000000000, -1.000000000000000000 ) ) ;
#37354=VECTOR ( 'NONE', #34089, 1000.000000000000000 ) ;
#37383=AXIS2_PLACEMENT_3D ( 'NONE', #67473, #39549, #55790 ) ;
#37396=CARTESIAN_POINT ( 'NONE',  ( 18.00000000000000000, 10.39230484541325161, -20.69999999999999929 ) ) ;
#37443=CONICAL_SURFACE ( 'NONE', #60305, 18.00000000000000355, 1.047197551196596965 ) ;
#37575=VERTEX_POINT ( 'NONE', #52782 ) ;
#37678=ADVANCED_FACE ( 'NONE', ( #60281 ), #54644, .F. ) ;
#37930=ORIENTED_EDGE ( 'NONE', *, *, #51872, .F. ) ;
#37945=FACE_OUTER_BOUND ( 'NONE', #44908, .T. ) ;
#38033=FACE_OUTER_BOUND ( 'NONE', #43709, .T. ) ;
#38109=VERTEX_POINT ( 'NONE', #6031 ) ;
#38337=CARTESIAN_POINT ( 'NONE',  ( 0.000000000000000000, 0.000000000000000000, 0.000000000000000000 ) ) ;
#38440=ORIENTED_EDGE ( 'NONE', *, *, #49584, .F. ) ;
#38449=EDGE_CURVE ( 'NONE', #46612, #33535, #14258, .T. ) ;
#38747=DIRECTION ( 'NONE',  ( -0.000000000000000000, -0.000000000000000000, -1.000000000000000000 ) ) ;
#38945=VERTEX_POINT ( 'NONE', #20779 ) ;
#39015=VERTEX_POINT ( 'NONE', #37396 ) ;
#39085=CARTESIAN_POINT ( 'NONE',  ( -18.00000000000000000, -10.39230484541329247, -1.607695154586745501 ) ) ;
#39105=VERTEX_POINT ( 'NONE', #50946 ) ;
#39123=ORIENTED_EDGE ( 'NONE', *, *, #34203, .F. ) ;
#39129=DIRECTION ( 'NONE',  ( 0.000000000000000000, 0.000000000000000000, -1.000000000000000000 ) ) ;
#39401=CARTESIAN_POINT ( 'NONE',  ( 18.00000000000000355, 0.000000000000000000, 0.000000000000000000 ) ) ;
#39423=ORIENTED_EDGE ( 'NONE', *, *, #31548, .T. ) ;
#39466=CARTESIAN_POINT ( 'NONE',  ( 9.000000000000014211, 15.58845726811988719, 0.000000000000000000 ) ) ;
#39549=DIRECTION ( 'NONE',  ( 0.5000000000000008882, 0.8660254037844381525, -0.000000000000000000 ) ) ;
#39579=CARTESIAN_POINT ( 'NONE',  ( -1.970469249063935269E-15, 20.78460969082654231, -21.50000000000000000 ) ) ;
#39600=ORIENTED_EDGE ( 'NONE', *, *, #53355, .F. ) ;
#39624=CIRCLE ( 'NONE', #7096, 18.00000000000000000 ) ;
#39722=LINE ( 'NONE', #1521, #37354 ) ;
#39949=DIRECTION ( 'NONE',  ( -0.8660254037844380415, -0.5000000000000012212, 0.000000000000000000 ) ) ;
#40017=CARTESIAN_POINT ( 'NONE',  ( 0.000000000000000000, 0.000000000000000000, -21.50000000000000000 ) ) ;
#40191=AXIS2_PLACEMENT_3D ( 'NONE', #27611, #49506, #50621 ) ;
#40471=CARTESIAN_POINT ( 'NONE',  ( -10.91045974869146029, -14.48545281793697548, -0.07476367467996689053 ) ) ;
#40503=CARTESIAN_POINT ( 'NONE',  ( -18.00000000000000000, 4.406054334071535905, -0.2960025734007523113 ) ) ;
#40741=SHAPE_REPRESENTATION_RELATIONSHIP ( 'NONE' , 'NONE' ,  #15137, #11994 ) ;
#40853=EDGE_CURVE ( 'NONE', #22710, #38109, #59701, .T. ) ;
#40964=ORIENTED_EDGE ( 'NONE', *, *, #30518, .T. ) ;
#41032=AXIS2_PLACEMENT_3D ( 'NONE', #70925, #42247, #59252 ) ;
#41033=DIRECTION ( 'NONE',  ( 0.000000000000000000, -1.000000000000000000, 0.000000000000000000 ) ) ;
#41221=AXIS2_PLACEMENT_3D ( 'NONE', #57330, #51656, #12035 ) ;
#41371=LINE ( 'NONE', #64380, #8551 ) ;
#41402=CARTESIAN_POINT ( 'NONE',  ( 5.197448530777795561, -17.78386138248279025, -0.2939692054342382121 ) ) ;
#41686=PLANE ( 'NONE',  #45422 ) ;
#41754=VERTEX_POINT ( 'NONE', #53410 ) ;
#41823=FACE_OUTER_BOUND ( 'NONE', #31772, .T. ) ;
#42054=CARTESIAN_POINT ( 'NONE',  ( 18.00000000000000355, 7.009507535100778952, -0.7186345456308858015 ) ) ;
#42121=CARTESIAN_POINT ( 'NONE',  ( 8.618100331995490748, -15.80894714424577607, -2.004418766382574114E-14 ) ) ;
#42180=FACE_BOUND ( 'NONE', #51368, .T. ) ;
#42195=EDGE_CURVE ( 'NONE', #24126, #8242, #69906, .T. ) ;
#42202=DIRECTION ( 'NONE',  ( 1.000000000000000000, 0.000000000000000000, 0.000000000000000000 ) ) ;
#42247=DIRECTION ( 'NONE',  ( -0.000000000000000000, -0.000000000000000000, 1.000000000000000000 ) ) ;
#42363=ORIENTED_EDGE ( 'NONE', *, *, #6311, .F. ) ;
#42487=VECTOR ( 'NONE', #6381, 1000.000000000000000 ) ;
#42773=AXIS2_PLACEMENT_3D ( 'NONE', #51181, #10082, #22127 ) ;
#42805=ORIENTED_EDGE ( 'NONE', *, *, #40853, .T. ) ;
#42858=CARTESIAN_POINT ( 'NONE',  ( 7.470240680701174085, -16.47166422291245524, -0.04683108270950198104 ) ) ;
#42932=ADVANCED_FACE ( 'NONE', ( #23787 ), #2255, .T. ) ;
#43273=CARTESIAN_POINT ( 'NONE',  ( -12.00000000000000355, 1.469576158976824342E-15, -25.03750572909317285 ) ) ;
#43321=ORIENTED_EDGE ( 'NONE', *, *, #43890, .T. ) ;
#43388=CIRCLE ( 'NONE', #18142, 18.00000000000000355 ) ;
#43468=ORIENTED_EDGE ( 'NONE', *, *, #68489, .T. ) ;
#43542=DIRECTION ( 'NONE',  ( -0.000000000000000000, -0.000000000000000000, -1.000000000000000000 ) ) ;
#43590=ORIENTED_EDGE ( 'NONE', *, *, #61700, .T. ) ;
#43615=CARTESIAN_POINT ( 'NONE',  ( -17.99999999999999645, -6.968949133139060947, -0.7423331077269027523 ) ) ;
#43634=FACE_OUTER_BOUND ( 'NONE', #15366, .T. ) ;
#43708=B_SPLINE_CURVE_WITH_KNOTS ( 'NONE', 3,
 ( #26679, #32360, #27058, #28173, #22498, #45520, #68536, #50070 ),
 .UNSPECIFIED., .F., .F.,
 ( 4, 2, 2, 4 ),
 ( 0.01854123755286043312, 0.02116956588062352679, 0.02379789420838662045, 0.02905455086391281125 ),
 .UNSPECIFIED. ) ;
#43709=EDGE_LOOP ( 'NONE', ( #6493, #10762, #22396 ) ) ;
#43817=ORIENTED_EDGE ( 'NONE', *, *, #44653, .T. ) ;
#43890=EDGE_CURVE ( 'NONE', #43896, #61876, #52079, .T. ) ;
#43896=VERTEX_POINT ( 'NONE', #69924 ) ;
#44047=AXIS2_PLACEMENT_3D ( 'NONE', #53066, #29318, #664 ) ;
#44227=EDGE_CURVE ( 'NONE', #71897, #1378, #47463, .T. ) ;
#44270=DIRECTION ( 'NONE',  ( -0.000000000000000000, -0.000000000000000000, 1.000000000000000000 ) ) ;
#44437=ORIENTED_EDGE ( 'NONE', *, *, #42195, .T. ) ;
#44633=DIRECTION ( 'NONE',  ( -1.000000000000000000, 0.000000000000000000, 0.000000000000000000 ) ) ;
#44653=EDGE_CURVE ( 'NONE', #35739, #64105, #11139, .T. ) ;
#44823=DIRECTION ( 'NONE',  ( 1.000000000000000000, 0.000000000000000000, 0.000000000000000000 ) ) ;
#44890=ORIENTED_EDGE ( 'NONE', *, *, #31548, .F. ) ;
#44908=EDGE_LOOP ( 'NONE', ( #1604, #16260, #36499, #755 ) ) ;
#44946=DIRECTION ( 'NONE',  ( 1.000000000000000000, -1.776356839400250465E-15, 0.000000000000000000 ) ) ;
#44977=ORIENTED_EDGE ( 'NONE', *, *, #31043, .T. ) ;
#44986=DIRECTION ( 'NONE',  ( 1.000000000000000000, 1.776356839400250465E-15, 0.000000000000000000 ) ) ;
#45005=EDGE_CURVE ( 'NONE', #20313, #46612, #48418, .T. ) ;
#45122=CARTESIAN_POINT ( 'NONE',  ( 18.00000000000000000, -10.39230484541328892, -20.69999999999999929 ) ) ;
#45203=EDGE_LOOP ( 'NONE', ( #65188, #2371, #52996, #43468 ) ) ;
#45366=DIRECTION ( 'NONE',  ( -0.000000000000000000, -0.000000000000000000, 1.000000000000000000 ) ) ;
#45406=CARTESIAN_POINT ( 'NONE',  ( -17.99999999999999645, 8.711927089654754042, -1.122611879773020682 ) ) ;
#45422=AXIS2_PLACEMENT_3D ( 'NONE', #30730, #35664, #977 ) ;
#45520=CARTESIAN_POINT ( 'NONE',  ( 18.00000000000000355, -3.500879649426325457, -0.1509495798675470069 ) ) ;
#45552=AXIS2_PLACEMENT_3D ( 'NONE', #9264, #33049, #56048 ) ;
#45577=ORIENTED_EDGE ( 'NONE', *, *, #53630, .F. ) ;
#45591=AXIS2_PLACEMENT_3D ( 'NONE', #16172, #74280, #72800 ) ;
#45752=ORIENTED_EDGE ( 'NONE', *, *, #61511, .T. ) ;
#45786=CARTESIAN_POINT ( 'NONE',  ( -17.99999999999999645, 3.528342445705423991, -0.1857217976155464134 ) ) ;
#45876=ADVANCED_FACE ( 'NONE', ( #42180, #41823 ), #30507, .T. ) ;
#45905=EDGE_CURVE ( 'NONE', #64105, #35739, #20640, .T. ) ;
#45933=CARTESIAN_POINT ( 'NONE',  ( 12.00000000000000355, 0.000000000000000000, -25.03750572909317285 ) ) ;
#45980=LINE ( 'NONE', #70481, #42487 ) ;
#46016=ADVANCED_FACE ( 'NONE', ( #38033 ), #60381, .T. ) ;
#46093=CARTESIAN_POINT ( 'NONE',  ( 0.000000000000000000, 0.000000000000000000, 0.000000000000000000 ) ) ;
#46299=EDGE_CURVE ( 'NONE', #39015, #64786, #2806, .T. ) ;
#46339=DIRECTION ( 'NONE',  ( 0.000000000000000000, 0.000000000000000000, 1.000000000000000000 ) ) ;
#46550=CARTESIAN_POINT ( 'NONE',  ( -8.234290096841624162, 16.03054008682954645, -0.009429105422156794022 ) ) ;
#46612=VERTEX_POINT ( 'NONE', #55247 ) ;
#46767=CONICAL_SURFACE ( 'NONE', #14237, 12.00000000000000178, 0.9599310885968795892 ) ;
#46791=DIRECTION ( 'NONE',  ( -1.000000000000000000, 0.000000000000000000, -0.000000000000000000 ) ) ;
#46867=ORIENTED_EDGE ( 'NONE', *, *, #13618, .T. ) ;
#46935=DIRECTION ( 'NONE',  ( 0.000000000000000000, 0.000000000000000000, -1.000000000000000000 ) ) ;
#47148=VECTOR ( 'NONE', #16003, 1000.000000000000000 ) ;
#47186=ORIENTED_EDGE ( 'NONE', *, *, #2034, .T. ) ;
#47463=LINE ( 'NONE', #36893, #1505 ) ;
#47516=CARTESIAN_POINT ( 'NONE',  ( 18.00000000000000000, 10.39230484541329247, -1.607695154586745501 ) ) ;
#47527=CARTESIAN_POINT ( 'NONE',  ( 0.000000000000000000, 0.000000000000000000, -21.50000000000000000 ) ) ;
#47595=CARTESIAN_POINT ( 'NONE',  ( -10.52975931929888453, -14.70525031332738664, -0.04683108270950248064 ) ) ;
#47648=CARTESIAN_POINT ( 'NONE',  ( -9.000000000000023093, 15.58845726811988541, 0.000000000000000000 ) ) ;
#47698=CARTESIAN_POINT ( 'NONE',  ( 18.00000000000000000, 10.39230484541325161, -20.69999999999999929 ) ) ;
#47711=DIRECTION ( 'NONE',  ( -0.000000000000000000, -0.000000000000000000, 1.000000000000000000 ) ) ;
#47816=EDGE_CURVE ( 'NONE', #72356, #19023, #21880, .T. ) ;
#48259=AXIS2_PLACEMENT_3D ( 'NONE', #40017, #51701, #18115 ) ;
#48345=ORIENTED_EDGE ( 'NONE', *, *, #19932, .F. ) ;
#48418=CIRCLE ( 'NONE', #60487, 10.50000000000000000 ) ;
#48521=CARTESIAN_POINT ( 'NONE',  ( 1.468605411411143757, -19.93670996121502625, -1.118160017449617349 ) ) ;
#48541=EDGE_CURVE ( 'NONE', #46612, #64105, #30394, .T. ) ;
#48676=EDGE_LOOP ( 'NONE', ( #2817, #30539 ) ) ;
#48805=AXIS2_PLACEMENT_3D ( 'NONE', #63154, #16743, #11481 ) ;
#48974=ORIENTED_EDGE ( 'NONE', *, *, #6431, .F. ) ;
#48988=ORIENTED_EDGE ( 'NONE', *, *, #51211, .T. ) ;
#48997=DIRECTION ( 'NONE',  ( -0.000000000000000000, -0.000000000000000000, 1.000000000000000000 ) ) ;
#49115=CARTESIAN_POINT ( 'NONE',  ( 0.000000000000000000, -20.78460969082658494, -20.69999999999999929 ) ) ;
#49156=VECTOR ( 'NONE', #18218, 1000.000000000000000 ) ;
#49247=EDGE_CURVE ( 'NONE', #7225, #6516, #68952, .T. ) ;
#49506=DIRECTION ( 'NONE',  ( 0.000000000000000000, 0.000000000000000000, 1.000000000000000000 ) ) ;
#49543=ORIENTED_EDGE ( 'NONE', *, *, #31043, .F. ) ;
#49584=EDGE_CURVE ( 'NONE', #39015, #34530, #7493, .T. ) ;
#49655=CARTESIAN_POINT ( 'NONE',  ( -18.00000000000000355, -3.500879649426325457, -0.1509495798675467015 ) ) ;
#49672=CARTESIAN_POINT ( 'NONE',  ( 0.000000000000000000, 0.000000000000000000, 0.000000000000000000 ) ) ;
#49864=CARTESIAN_POINT ( 'NONE',  ( -9.000000000000035527, -15.58845726811991739, -20.69999999999999929 ) ) ;
#49922=DIRECTION ( 'NONE',  ( 1.000000000000000000, 0.000000000000000000, 0.000000000000000000 ) ) ;
#49999=CARTESIAN_POINT ( 'NONE',  ( -18.00000000000000000, 10.39230484541324628, -20.69999999999999929 ) ) ;
#50007=ORIENTED_EDGE ( 'NONE', *, *, #44653, .F. ) ;
#50009=VECTOR ( 'NONE', #58754, 1000.000000000000000 ) ;
#50066=PLANE ( 'NONE',  #22258 ) ;
#50070=CARTESIAN_POINT ( 'NONE',  ( 18.00000000000000355, 0.000000000000000000, 0.000000000000000000 ) ) ;
#50155=FACE_OUTER_BOUND ( 'NONE', #35105, .T. ) ;
#50199=( NAMED_UNIT ( * ) SI_UNIT ( $, .STERADIAN. ) SOLID_ANGLE_UNIT ( ) );
#50352=ADVANCED_FACE ( 'NONE', ( #59367 ), #53335, .T. ) ;
#50454=AXIS2_PLACEMENT_3D ( 'NONE', #3654, #54228, #31579 ) ;
#50621=DIRECTION ( 'NONE',  ( 1.000000000000000000, 0.000000000000000000, -0.000000000000000000 ) ) ;
#50711=DIRECTION ( 'NONE',  ( 0.8660254037844379305, 0.5000000000000011102, 0.000000000000000000 ) ) ;
#50732=ORIENTED_EDGE ( 'NONE', *, *, #44227, .F. ) ;
#50775=CARTESIAN_POINT ( 'NONE',  ( 18.00000000000000000, 10.39230484541329247, -1.607695154586745501 ) ) ;
#50783=DIRECTION ( 'NONE',  ( 0.000000000000000000, 0.000000000000000000, -1.000000000000000000 ) ) ;
#50805=AXIS2_PLACEMENT_3D ( 'NONE', #19889, #30483, #65915 ) ;
#50807=EDGE_LOOP ( 'NONE', ( #3884, #62065, #48345 ) ) ;
#50862=ORIENTED_EDGE ( 'NONE', *, *, #23566, .T. ) ;
#50919=EDGE_CURVE ( 'NONE', #41754, #43896, #58156, .T. ) ;
#50946=CARTESIAN_POINT ( 'NONE',  ( -9.000000000000023093, 15.58845726811988541, 0.000000000000000000 ) ) ;
#51075=CARTESIAN_POINT ( 'NONE',  ( 18.00000000000000000, -10.39230484541328892, -21.50000000000000000 ) ) ;
#51124=CIRCLE ( 'NONE', #21012, 18.00000000000000000 ) ;
#51129=CARTESIAN_POINT ( 'NONE',  ( 12.00000000000000178, 1.469576158976824144E-15, -21.47459999999999525 ) ) ;
#51141=ORIENTED_EDGE ( 'NONE', *, *, #16399, .F. ) ;
#51152=CARTESIAN_POINT ( 'NONE',  ( 12.04876049975178631, 13.82825457289349558, -0.1850551574587529224 ) ) ;
#51181=CARTESIAN_POINT ( 'NONE',  ( 0.000000000000000000, 0.000000000000000000, -20.69999999999999929 ) ) ;
#51211=EDGE_CURVE ( 'NONE', #51876, #61876, #3417, .T. ) ;
#51219=CARTESIAN_POINT ( 'NONE',  ( -5.952395412842847122, -17.34799259689866702, -0.1532218116813779951 ) ) ;
#51264=ORIENTED_EDGE ( 'NONE', *, *, #66753, .T. ) ;
#51270=PLANE ( 'NONE',  #45591 ) ;
#51368=EDGE_LOOP ( 'NONE', ( #36519, #32655 ) ) ;
#51394=CARTESIAN_POINT ( 'NONE',  ( 1.502314598737163567E-15, -20.78460969082658494, -21.50000000000000000 ) ) ;
#51449=DIRECTION ( 'NONE',  ( 0.8660254037844379305, 0.5000000000000011102, 0.000000000000000000 ) ) ;
#51456=LINE ( 'NONE', #39401, #47148 ) ;
#51571=DIRECTION ( 'NONE',  ( 0.000000000000000000, -1.000000000000000000, 0.000000000000000000 ) ) ;
#51583=VERTEX_POINT ( 'NONE', #1768 ) ;
#51585=PRODUCT_DEFINITION_CONTEXT ( 'detailed design', #60674, 'design' ) ;
#51610=EDGE_CURVE ( 'NONE', #26967, #38945, #53447, .T. ) ;
#51656=DIRECTION ( 'NONE',  ( -0.000000000000000000, -0.000000000000000000, 1.000000000000000000 ) ) ;
#51701=DIRECTION ( 'NONE',  ( -0.000000000000000000, -0.000000000000000000, -1.000000000000000000 ) ) ;
#51738=ADVANCED_FACE ( 'NONE', ( #14164 ), #31536, .T. ) ;
#51829=CARTESIAN_POINT ( 'NONE',  ( 1.502314598737163567E-15, -20.78460969082658494, -20.69999999999999929 ) ) ;
#51872=EDGE_CURVE ( 'NONE', #20252, #41754, #18450, .T. ) ;
#51876=VERTEX_POINT ( 'NONE', #49999 ) ;
#51958=DIRECTION ( 'NONE',  ( 1.000000000000000000, 0.000000000000000000, 0.000000000000000000 ) ) ;
#51967=ADVANCED_FACE ( 'NONE', ( #52240 ), #382, .T. ) ;
#52009=FACE_OUTER_BOUND ( 'NONE', #57247, .T. ) ;
#52079=B_SPLINE_CURVE_WITH_KNOTS ( 'NONE', 3,
 ( #28804, #57873, #17105, #45786, #40503, #28062, #45406, #35594 ),
 .UNSPECIFIED., .F., .F.,
 ( 4, 2, 2, 4 ),
 ( 0.02905455086391281472, 0.03168444077422613581, 0.03431433068453945689, 0.03957411050516609907 ),
 .UNSPECIFIED. ) ;
#52172=CARTESIAN_POINT ( 'NONE',  ( -16.53139458858884581, -11.24020457502486892, -1.118160017449591814 ) ) ;
#52240=FACE_OUTER_BOUND ( 'NONE', #9083, .T. ) ;
#52267=EDGE_CURVE ( 'NONE', #17730, #24196, #65392, .T. ) ;
#52367=CARTESIAN_POINT ( 'NONE',  ( -10.53333261448112346, 14.70318727039197881, 2.005774019098183203E-15 ) ) ;
#52392=ORIENTED_EDGE ( 'NONE', *, *, #59046, .T. ) ;
#52506=AXIS2_PLACEMENT_3D ( 'NONE', #73678, #44270, #49922 ) ;
#52782=CARTESIAN_POINT ( 'NONE',  ( -12.00000000000000355, 1.469576158976824342E-15, -21.50000000000000000 ) ) ;
#52814=ORIENTED_EDGE ( 'NONE', *, *, #14412, .T. ) ;
#52875=ORIENTED_EDGE ( 'NONE', *, *, #4838, .F. ) ;
#52993=EDGE_CURVE ( 'NONE', #20252, #8242, #66926, .T. ) ;
#52996=ORIENTED_EDGE ( 'NONE', *, *, #71458, .T. ) ;
#53066=CARTESIAN_POINT ( 'NONE',  ( 0.000000000000000000, 0.000000000000000000, 0.000000000000000000 ) ) ;
#53331=CARTESIAN_POINT ( 'NONE',  ( -7.470240680701166980, 16.47166422291241616, -0.04683108270947877738 ) ) ;
#53335=PLANE ( 'NONE',  #30448 ) ;
#53355=EDGE_CURVE ( 'NONE', #62930, #19023, #66791, .T. ) ;
#53397=CARTESIAN_POINT ( 'NONE',  ( 18.00000000000000355, 0.000000000000000000, 0.000000000000000000 ) ) ;
#53399=AXIS2_PLACEMENT_3D ( 'NONE', #15656, #10389, #9267 ) ;
#53410=CARTESIAN_POINT ( 'NONE',  ( -9.000000000000017764, -15.58845726811988719, 0.000000000000000000 ) ) ;
#53447=LINE ( 'NONE', #64757, #16005 ) ;
#53471=ORIENTED_EDGE ( 'NONE', *, *, #19767, .F. ) ;
#53629=CIRCLE ( 'NONE', #42773, 18.00000000000000355 ) ;
#53630=EDGE_CURVE ( 'NONE', #61876, #39105, #28972, .T. ) ;
#54165=DIRECTION ( 'NONE',  ( -0.000000000000000000, -0.000000000000000000, 1.000000000000000000 ) ) ;
#54228=DIRECTION ( 'NONE',  ( -0.5000000000000009992, -0.8660254037844380415, 0.000000000000000000 ) ) ;
#54609=DIRECTION ( 'NONE',  ( -0.000000000000000000, -0.000000000000000000, 1.000000000000000000 ) ) ;
#54644=CYLINDRICAL_SURFACE ( 'NONE', #17662, 12.00000000000000355 ) ;
#54910=CARTESIAN_POINT ( 'NONE',  ( 0.000000000000000000, 0.000000000000000000, -20.42428869268542968 ) ) ;
#55002=FACE_OUTER_BOUND ( 'NONE', #63439, .T. ) ;
#55082=PRODUCT_DEFINITION_FORMATION_WITH_SPECIFIED_SOURCE ( 'ANY', '', #8304, .NOT_KNOWN. ) ;
#55129=AXIS2_PLACEMENT_3D ( 'NONE', #4587, #57017, #44946 ) ;
#55169=DIRECTION ( 'NONE',  ( -0.8660254037844380415, -0.5000000000000012212, 0.000000000000000000 ) ) ;
#55247=CARTESIAN_POINT ( 'NONE',  ( -10.50000000000000000, 1.285879139104720831E-15, -20.42428869268542968 ) ) ;
#55347=CARTESIAN_POINT ( 'NONE',  ( 16.52771754582130015, -11.24232751665652508, -1.116934336526976379 ) ) ;
#55381=EDGE_CURVE ( 'NONE', #51876, #38945, #7211, .T. ) ;
#55451=CARTESIAN_POINT ( 'NONE',  ( -18.00000000000000000, -10.39230484541329247, -1.607695154586745501 ) ) ;
#55592=CIRCLE ( 'NONE', #11000, 18.00000000000000355 ) ;
#55621=EDGE_CURVE ( 'NONE', #46612, #20313, #19193, .T. ) ;
#55664=ORIENTED_EDGE ( 'NONE', *, *, #49247, .T. ) ;
#55790=DIRECTION ( 'NONE',  ( -0.8660254037844381525, 0.5000000000000008882, 0.000000000000000000 ) ) ;
#55823=DIRECTION ( 'NONE',  ( 0.000000000000000000, 0.000000000000000000, 1.000000000000000000 ) ) ;
#55978=DIRECTION ( 'NONE',  ( 0.000000000000000000, 0.000000000000000000, -1.000000000000000000 ) ) ;
#56048=DIRECTION ( 'NONE',  ( -1.000000000000000000, 0.000000000000000000, 0.000000000000000000 ) ) ;
#56086=CARTESIAN_POINT ( 'NONE',  ( 15.05053643744962777, 12.09517842721670355, -0.7140392532422370486 ) ) ;
#56094=ORIENTED_EDGE ( 'NONE', *, *, #50919, .F. ) ;
#56298=FACE_OUTER_BOUND ( 'NONE', #60011, .T. ) ;
#56308=EDGE_CURVE ( 'NONE', #70823, #24126, #39722, .T. ) ;
#56340=ORIENTED_EDGE ( 'NONE', *, *, #38449, .T. ) ;
#56383=ORIENTED_EDGE ( 'NONE', *, *, #74544, .T. ) ;
#56386=LINE ( 'NONE', #27700, #26629 ) ;
#56435=AXIS2_PLACEMENT_3D ( 'NONE', #24386, #58735, #51958 ) ;
#56453=CARTESIAN_POINT ( 'NONE',  ( 10.52975931929885789, 14.70525031332736177, -0.04683108270947845125 ) ) ;
#56803=LINE ( 'NONE', #51129, #68177 ) ;
#56861=CARTESIAN_POINT ( 'NONE',  ( 0.000000000000000000, 0.000000000000000000, -1.050311307314560239 ) ) ;
#57017=DIRECTION ( 'NONE',  ( -0.000000000000000000, -0.000000000000000000, -1.000000000000000000 ) ) ;
#57129=ORIENTED_EDGE ( 'NONE', *, *, #51211, .F. ) ;
#57168=VECTOR ( 'NONE', #11907, 1000.000000000000000 ) ;
#57247=EDGE_LOOP ( 'NONE', ( #66786, #17987, #50007, #6321 ) ) ;
#57266=CARTESIAN_POINT ( 'NONE',  ( -2.955318825516840775, -19.07835557137326532, -0.7126204852947463086 ) ) ;
#57291=CARTESIAN_POINT ( 'NONE',  ( -16.52771754582129660, 11.24232751665648422, -1.116934336526962390 ) ) ;
#57306=DIRECTION ( 'NONE',  ( 0.000000000000000000, 0.000000000000000000, -1.000000000000000000 ) ) ;
#57330=CARTESIAN_POINT ( 'NONE',  ( 0.000000000000000000, 0.000000000000000000, -20.69999999999999929 ) ) ;
#57354=AXIS2_PLACEMENT_3D ( 'NONE', #63097, #11422, #34459 ) ;
#57873=CARTESIAN_POINT ( 'NONE',  ( -18.00000000000000355, 0.8785859941773035420, 1.985868744837707145E-15 ) ) ;
#58156=CIRCLE ( 'NONE', #17195, 18.00000000000000000 ) ;
#58175=ORIENTED_EDGE ( 'NONE', *, *, #71726, .T. ) ;
#58279=ORIENTED_EDGE ( 'NONE', *, *, #11448, .T. ) ;
#58575=CARTESIAN_POINT ( 'NONE',  ( -12.04876049975181296, -13.82825457289352755, -0.1850551574587747938 ) ) ;
#58674=ORIENTED_EDGE ( 'NONE', *, *, #56308, .T. ) ;
#58735=DIRECTION ( 'NONE',  ( -0.000000000000000000, -0.000000000000000000, 1.000000000000000000 ) ) ;
#58754=DIRECTION ( 'NONE',  ( -0.000000000000000000, -0.000000000000000000, 1.000000000000000000 ) ) ;
#58758=CARTESIAN_POINT ( 'NONE',  ( 0.000000000000000000, 0.000000000000000000, 0.000000000000000000 ) ) ;
#58916=AXIS2_PLACEMENT_3D ( 'NONE', #10086, #73084, #21392 ) ;
#58924=ORIENTED_EDGE ( 'NONE', *, *, #66753, .F. ) ;
#59000=CARTESIAN_POINT ( 'NONE',  ( -8.618100331995474761, 15.80894714424573344, 2.003974074085267026E-15 ) ) ;
#59046=EDGE_CURVE ( 'NONE', #26967, #728, #35066, .T. ) ;
#59128=PLANE ( 'NONE',  #22149 ) ;
#59191=DIRECTION ( 'NONE',  ( 1.000000000000000000, 0.000000000000000000, 0.000000000000000000 ) ) ;
#59224=CARTESIAN_POINT ( 'NONE',  ( -5.204170427930421283E-15, 20.78460969082654231, -1.607695154586745501 ) ) ;
#59252=DIRECTION ( 'NONE',  ( 1.000000000000000000, 0.000000000000000000, 0.000000000000000000 ) ) ;
#59367=FACE_OUTER_BOUND ( 'NONE', #2946, .T. ) ;
#59408=ORIENTED_EDGE ( 'NONE', *, *, #45005, .T. ) ;
#59424=CARTESIAN_POINT ( 'NONE',  ( 17.99999999999999645, 3.528342445705438202, -0.1857217976155470518 ) ) ;
#59462=CARTESIAN_POINT ( 'NONE',  ( -12.00000000000000000, 1.469576158976823947E-15, 6.938893903907228378E-15 ) ) ;
#59527=LINE ( 'NONE', #43273, #73768 ) ;
#59628=EDGE_LOOP ( 'NONE', ( #52814, #68219, #64763, #62091, #40964, #20096 ) ) ;
#59701=LINE ( 'NONE', #66463, #4541 ) ;
#59762=DIRECTION ( 'NONE',  ( 0.8191520442889907994, 1.003171929053523514E-16, -0.5735764363510474917 ) ) ;
#59893=DIRECTION ( 'NONE',  ( -0.000000000000000000, -0.000000000000000000, 1.000000000000000000 ) ) ;
#59948=CARTESIAN_POINT ( 'NONE',  ( 1.472282454178701849, 19.93458701958330082, -1.116934336526971272 ) ) ;
#60011=EDGE_LOOP ( 'NONE', ( #34362, #52392 ) ) ;
#60167=CARTESIAN_POINT ( 'NONE',  ( -10.50000000000000000, 1.285879139104720831E-15, -21.50000000000000000 ) ) ;
#60210=DIRECTION ( 'NONE',  ( 0.8660254037844380415, -0.5000000000000009992, 0.000000000000000000 ) ) ;
#60281=FACE_OUTER_BOUND ( 'NONE', #45203, .T. ) ;
#60305=AXIS2_PLACEMENT_3D ( 'NONE', #49672, #50783, #61742 ) ;
#60315=CARTESIAN_POINT ( 'NONE',  ( 9.000000000000014211, 15.58845726811988719, 0.000000000000000000 ) ) ;
#60381=CONICAL_SURFACE ( 'NONE', #12357, 18.00000000000000355, 1.047197551196596965 ) ;
#60415=ADVANCED_FACE ( 'NONE', ( #70735 ), #46767, .F. ) ;
#60487=AXIS2_PLACEMENT_3D ( 'NONE', #54910, #54165, #14140 ) ;
#60497=FACE_OUTER_BOUND ( 'NONE', #64623, .T. ) ;
#60504=ADVANCED_FACE ( 'NONE', ( #52009 ), #347, .F. ) ;
#60556=AXIS2_PLACEMENT_3D ( 'NONE', #7131, #2204, #25569 ) ;
#60674=APPLICATION_CONTEXT ( 'automotive_design' ) ;
#60702=B_SPLINE_CURVE_WITH_KNOTS ( 'NONE', 3,
 ( #53397, #30378, #24340, #59424, #19050, #42054, #25062, #2444 ),
 .UNSPECIFIED., .F., .F.,
 ( 4, 2, 2, 4 ),
 ( 0.02905455086391281125, 0.03168444077422614275, 0.03431433068453947771, 0.03957411050516614071 ),
 .UNSPECIFIED. ) ;
#60982=FACE_OUTER_BOUND ( 'NONE', #63428, .T. ) ;
#61059=FACE_OUTER_BOUND ( 'NONE', #70845, .T. ) ;
#61162=ADVANCED_FACE ( 'NONE', ( #50155 ), #51270, .F. ) ;
#61409=CARTESIAN_POINT ( 'NONE',  ( 0.000000000000000000, 0.000000000000000000, 0.000000000000000000 ) ) ;
#61496=AXIS2_PLACEMENT_3D ( 'NONE', #27399, #38747, #72308 ) ;
#61511=EDGE_CURVE ( 'NONE', #39105, #19023, #39624, .T. ) ;
#61544=ADVANCED_FACE ( 'NONE', ( #55002 ), #68166, .T. ) ;
#61624=EDGE_LOOP ( 'NONE', ( #37098, #50862, #45577 ) ) ;
#61700=EDGE_CURVE ( 'NONE', #70161, #72356, #43708, .T. ) ;
#61742=DIRECTION ( 'NONE',  ( -1.000000000000000000, 0.000000000000000000, 0.000000000000000000 ) ) ;
#61769=DIRECTION ( 'NONE',  ( 1.000000000000000000, 0.000000000000000000, 0.000000000000000000 ) ) ;
#61809=PLANE ( 'NONE',  #37383 ) ;
#61823=DIRECTION ( 'NONE',  ( 1.000000000000000000, 0.000000000000000000, 0.000000000000000000 ) ) ;
#61876=VERTEX_POINT ( 'NONE', #70035 ) ;
#62065=ORIENTED_EDGE ( 'NONE', *, *, #55381, .F. ) ;
#62084=DIRECTION ( 'NONE',  ( 1.000000000000000000, 0.000000000000000000, 0.000000000000000000 ) ) ;
#62090=CARTESIAN_POINT ( 'NONE',  ( -18.00000000000000000, -6.103439543526007149, -0.5706341627281755757 ) ) ;
#62091=ORIENTED_EDGE ( 'NONE', *, *, #42195, .F. ) ;
#62107=CARTESIAN_POINT ( 'NONE',  ( 9.000000000000023093, -15.58845726811988541, 0.000000000000000000 ) ) ;
#62574=CARTESIAN_POINT ( 'NONE',  ( -1.970469249063935269E-15, 20.78460969082654231, -20.69999999999999929 ) ) ;
#62706=FACE_OUTER_BOUND ( 'NONE', #59628, .T. ) ;
#62722=EDGE_LOOP ( 'NONE', ( #46867, #35083, #22342, #33166 ) ) ;
#62807=AXIS2_PLACEMENT_3D ( 'NONE', #6762, #31244, #59191 ) ;
#62817=DIRECTION ( 'NONE',  ( -1.000000000000000000, 0.000000000000000000, -0.000000000000000000 ) ) ;
#62821=CIRCLE ( 'NONE', #61496, 12.00000000000000355 ) ;
#62930=VERTEX_POINT ( 'NONE', #4167 ) ;
#63097=CARTESIAN_POINT ( 'NONE',  ( 0.000000000000000000, 0.000000000000000000, 0.000000000000000000 ) ) ;
#63154=CARTESIAN_POINT ( 'NONE',  ( 0.000000000000000000, 0.000000000000000000, -1.155342438046016218 ) ) ;
#63274=CARTESIAN_POINT ( 'NONE',  ( -7.285838599102589797E-14, -20.78460969082654231, -1.607695154586745501 ) ) ;
#63314=CARTESIAN_POINT ( 'NONE',  ( 0.000000000000000000, 0.000000000000000000, -21.47459999999999525 ) ) ;
#63428=EDGE_LOOP ( 'NONE', ( #43590, #63471, #9557 ) ) ;
#63439=EDGE_LOOP ( 'NONE', ( #27441, #51141, #55664 ) ) ;
#63471=ORIENTED_EDGE ( 'NONE', *, *, #11842, .T. ) ;
#63510=CYLINDRICAL_SURFACE ( 'NONE', #41032, 12.00000000000000355 ) ;
#63672=CARTESIAN_POINT ( 'NONE',  ( -18.00000000000000000, 10.39230484541324628, -1.607695154586745501 ) ) ;
#64054=CARTESIAN_POINT ( 'NONE',  ( -9.000000000000023093, 15.58845726811988541, 0.000000000000000000 ) ) ;
#64105=VERTEX_POINT ( 'NONE', #25398 ) ;
#64204=EDGE_LOOP ( 'NONE', ( #44437, #30379, #70506, #50732, #56383, #58674 ) ) ;
#64214=AXIS2_PLACEMENT_3D ( 'NONE', #574, #46935, #5475 ) ;
#64277=CARTESIAN_POINT ( 'NONE',  ( -5.951239500248230563, 17.34865996334628946, -0.1850551574587545600 ) ) ;
#64330=LINE ( 'NONE', #7360, #57168 ) ;
#64366=CARTESIAN_POINT ( 'NONE',  ( 10.50000000000000000, 0.000000000000000000, -1.050311307314560239 ) ) ;
#64380=CARTESIAN_POINT ( 'NONE',  ( 10.50000000000000000, 0.000000000000000000, -21.50000000000000000 ) ) ;
#64391=VECTOR ( 'NONE', #41033, 1000.000000000000000 ) ;
#64623=EDGE_LOOP ( 'NONE', ( #13334, #52875, #19340 ) ) ;
#64647=CARTESIAN_POINT ( 'NONE',  ( -2.949463562550372231, 19.08173610902309036, -0.7140392532422442651 ) ) ;
#64649=ORIENTED_EDGE ( 'NONE', *, *, #46299, .T. ) ;
#64757=CARTESIAN_POINT ( 'NONE',  ( -18.00000000000000355, 2.204364238465235822E-15, 0.000000000000000000 ) ) ;
#64763=ORIENTED_EDGE ( 'NONE', *, *, #52993, .T. ) ;
#64772=LINE ( 'NONE', #11608, #64391 ) ;
#64786=VERTEX_POINT ( 'NONE', #16980 ) ;
#64810=DIRECTION ( 'NONE',  ( 1.000000000000000000, 0.000000000000000000, 0.000000000000000000 ) ) ;
#65133=CARTESIAN_POINT ( 'NONE',  ( 8.234290096841634821, -16.03054008682958198, -0.009429105422179598697 ) ) ;
#65188=ORIENTED_EDGE ( 'NONE', *, *, #20371, .F. ) ;
#65243=AXIS2_PLACEMENT_3D ( 'NONE', #51394, #16676, #16302 ) ;
#65376=CARTESIAN_POINT ( 'NONE',  ( -1.468605411411171291, 19.93670996121496586, -1.118160017449583155 ) ) ;
#65392=CIRCLE ( 'NONE', #19605, 12.00000000000000000 ) ;
#65418=MANIFOLD_SOLID_BREP ( 'EndChamfer', #69574 ) ;
#65511=CARTESIAN_POINT ( 'NONE',  ( 7.089540251308593888, -16.69146171830286463, -0.07476367467996772320 ) ) ;
#65549=LINE ( 'NONE', #8958, #9979 ) ;
#65578=AXIS2_PLACEMENT_3D ( 'NONE', #14643, #19200, #42202 ) ;
#65721=CARTESIAN_POINT ( 'NONE',  ( 0.000000000000000000, 0.000000000000000000, -1.155342438046016218 ) ) ;
#65763=DIRECTION ( 'NONE',  ( -0.000000000000000000, -0.000000000000000000, 1.000000000000000000 ) ) ;
#65773=VECTOR ( 'NONE', #60210, 1000.000000000000000 ) ;
#65856=EDGE_CURVE ( 'NONE', #37575, #51583, #16182, .T. ) ;
#65915=DIRECTION ( 'NONE',  ( 1.000000000000000000, 0.000000000000000000, 0.000000000000000000 ) ) ;
#66227=AXIS2_PLACEMENT_3D ( 'NONE', #47527, #18868, #69444 ) ;
#66236=ADVANCED_FACE ( 'NONE', ( #60497 ), #71640, .T. ) ;
#66248=DIRECTION ( 'NONE',  ( -0.8191520442889911324, 1.003171929053523884E-16, 0.5735764363510471586 ) ) ;
#66295=ORIENTED_EDGE ( 'NONE', *, *, #3283, .F. ) ;
#66463=CARTESIAN_POINT ( 'NONE',  ( -1.970469249063935269E-15, 20.78460969082654231, -20.69999999999999929 ) ) ;
#66512=ADVANCED_FACE ( 'NONE', ( #60982 ), #11414, .T. ) ;
#66753=EDGE_CURVE ( 'NONE', #19023, #34530, #73108, .T. ) ;
#66786=ORIENTED_EDGE ( 'NONE', *, *, #55621, .F. ) ;
#66788=DIRECTION ( 'NONE',  ( 0.000000000000000000, 0.000000000000000000, 1.000000000000000000 ) ) ;
#66791=B_SPLINE_CURVE_WITH_KNOTS ( 'NONE', 3,
 ( #59224, #59948, #9017, #13534, #8263, #60315 ),
 .UNSPECIFIED., .F., .F.,
 ( 4, 2, 4 ),
 ( 2.380728322736233691E-07, 0.005257893135091050787, 0.01051554819734982701 ),
 .UNSPECIFIED. ) ;
#66919=CIRCLE ( 'NONE', #52506, 12.00000000000000178 ) ;
#66926=B_SPLINE_CURVE_WITH_KNOTS ( 'NONE', 3,
 ( #1059, #42121, #65133, #42858, #65511, #13444, #41402, #36851, #48521, #7442 ),
 .UNSPECIFIED., .F., .F.,
 ( 4, 2, 2, 2, 4 ),
 ( 0.01051554819734976456, 0.01182504667393342521, 0.01313454515051708585, 0.01575354210368440713, 0.02099153601001905317 ),
 .UNSPECIFIED. ) ;
#67175=EDGE_LOOP ( 'NONE', ( #71064, #71367, #12610, #68402, #49543, #42363 ) ) ;
#67473=CARTESIAN_POINT ( 'NONE',  ( 18.00000000000000000, 10.39230484541325161, -21.50000000000000000 ) ) ;
#67652=CARTESIAN_POINT ( 'NONE',  ( -18.00000000000000000, -10.39230484541329425, -20.69999999999999929 ) ) ;
#67678=EDGE_CURVE ( 'NONE', #8242, #41754, #2957, .T. ) ;
#67748=AXIS2_PLACEMENT_3D ( 'NONE', #69364, #18052, #64810 ) ;
#67753=FACE_OUTER_BOUND ( 'NONE', #23473, .T. ) ;
#68166=PLANE ( 'NONE',  #58916 ) ;
#68177=VECTOR ( 'NONE', #59762, 1000.000000000000114 ) ;
#68183=EDGE_CURVE ( 'NONE', #20313, #31504, #56803, .T. ) ;
#68219=ORIENTED_EDGE ( 'NONE', *, *, #6088, .T. ) ;
#68364=ORIENTED_EDGE ( 'NONE', *, *, #68489, .F. ) ;
#68402=ORIENTED_EDGE ( 'NONE', *, *, #49247, .F. ) ;
#68447=ORIENTED_EDGE ( 'NONE', *, *, #1666, .F. ) ;
#68489=EDGE_CURVE ( 'NONE', #31504, #33535, #66919, .T. ) ;
#68536=CARTESIAN_POINT ( 'NONE',  ( 18.00000000000000000, -1.756128610415474078, 2.107417972768699244E-15 ) ) ;
#68666=( NAMED_UNIT ( * ) PLANE_ANGLE_UNIT ( ) SI_UNIT ( $, .RADIAN. ) );
#68952=CIRCLE ( 'NONE', #41221, 18.00000000000000355 ) ;
#69174=DIRECTION ( 'NONE',  ( 0.000000000000000000, 0.000000000000000000, 1.000000000000000000 ) ) ;
#69199=MECHANICAL_DESIGN_GEOMETRIC_PRESENTATION_REPRESENTATION('',(#72810),#22224);
#69364=CARTESIAN_POINT ( 'NONE',  ( 0.000000000000000000, 0.000000000000000000, -21.47459999999999525 ) ) ;
#69417=( NAMED_UNIT ( * ) PLANE_ANGLE_UNIT ( ) SI_UNIT ( $, .RADIAN. ) );
#69444=DIRECTION ( 'NONE',  ( 1.000000000000000000, 0.000000000000000000, 0.000000000000000000 ) ) ;
#69574=CLOSED_SHELL ( 'NONE', ( #14538, #32480, #72336, #11350, #60504, #29801, #71754, #4207, #61162, #18729, #35306, #22555, #45876, #9113, #20542, #61544, #51738, #11516, #42932, #69724, #50352, #51967, #5985, #73482, #66236, #46016, #66512, #32966, #60415, #37678 ) ) ;
#69701=CYLINDRICAL_SURFACE ( 'NONE', #22191, 18.00000000000000355 ) ;
#69724=ADVANCED_FACE ( 'NONE', ( #72776 ), #4122, .T. ) ;
#69906=LINE ( 'NONE', #70632, #49156 ) ;
#69924=CARTESIAN_POINT ( 'NONE',  ( -18.00000000000000355, 0.000000000000000000, 0.000000000000000000 ) ) ;
#70035=CARTESIAN_POINT ( 'NONE',  ( -18.00000000000000000, 10.39230484541324628, -1.607695154586745501 ) ) ;
#70161=VERTEX_POINT ( 'NONE', #22377 ) ;
#70260=CARTESIAN_POINT ( 'NONE',  ( -9.000000000000017764, -15.58845726811988719, 0.000000000000000000 ) ) ;
#70315=DIRECTION ( 'NONE',  ( -1.000000000000000000, 0.000000000000000000, -0.000000000000000000 ) ) ;
#70481=CARTESIAN_POINT ( 'NONE',  ( 18.00000000000000000, 10.39230484541325161, -20.69999999999999929 ) ) ;
#70506=ORIENTED_EDGE ( 'NONE', *, *, #21299, .T. ) ;
#70632=CARTESIAN_POINT ( 'NONE',  ( 1.502314598737163567E-15, -20.78460969082658494, -21.50000000000000000 ) ) ;
#70719=DIRECTION ( 'NONE',  ( -0.8660254037844381525, 0.5000000000000008882, 0.000000000000000000 ) ) ;
#70735=FACE_OUTER_BOUND ( 'NONE', #35090, .T. ) ;
#70823=VERTEX_POINT ( 'NONE', #49864 ) ;
#70845=EDGE_LOOP ( 'NONE', ( #7684, #2509, #51264, #38440, #64649, #72045 ) ) ;
#70890=EDGE_LOOP ( 'NONE', ( #58175, #7163, #68447 ) ) ;
#70914=CARTESIAN_POINT ( 'NONE',  ( 0.000000000000000000, 30.78460969082653875, -20.69999999999999929 ) ) ;
#70925=CARTESIAN_POINT ( 'NONE',  ( 0.000000000000000000, 0.000000000000000000, -25.03750572909317285 ) ) ;
#71064=ORIENTED_EDGE ( 'NONE', *, *, #51610, .F. ) ;
#71196=CARTESIAN_POINT ( 'NONE',  ( 10.50000000000000000, 0.000000000000000000, -20.42428869268542968 ) ) ;
#71206=DIRECTION ( 'NONE',  ( 1.000000000000000000, 1.776356839400250465E-15, 0.000000000000000000 ) ) ;
#71367=ORIENTED_EDGE ( 'NONE', *, *, #14265, .F. ) ;
#71458=EDGE_CURVE ( 'NONE', #51583, #31504, #18011, .T. ) ;
#71640=CONICAL_SURFACE ( 'NONE', #9030, 18.00000000000000355, 1.047197551196596965 ) ;
#71726=EDGE_CURVE ( 'NONE', #64786, #38109, #53629, .T. ) ;
#71754=ADVANCED_FACE ( 'NONE', ( #27054 ), #50066, .T. ) ;
#71897=VERTEX_POINT ( 'NONE', #6291 ) ;
#71966=DIRECTION ( 'NONE',  ( -1.000000000000000000, 0.000000000000000000, 0.000000000000000000 ) ) ;
#71997=ORIENTED_EDGE ( 'NONE', *, *, #56308, .F. ) ;
#72027=ORIENTED_EDGE ( 'NONE', *, *, #61511, .F. ) ;
#72045=ORIENTED_EDGE ( 'NONE', *, *, #1666, .T. ) ;
#72121=EDGE_LOOP ( 'NONE', ( #72620, #35732, #16359, #15259 ) ) ;
#72308=DIRECTION ( 'NONE',  ( 1.000000000000000000, 0.000000000000000000, 0.000000000000000000 ) ) ;
#72336=ADVANCED_FACE ( 'NONE', ( #36256 ), #27116, .F. ) ;
#72356=VERTEX_POINT ( 'NONE', #17125 ) ;
#72470=AXIS2_PLACEMENT_3D ( 'NONE', #72602, #43542, #2449 ) ;
#72572=CARTESIAN_POINT ( 'NONE',  ( 0.000000000000000000, 0.000000000000000000, 0.000000000000000000 ) ) ;
#72602=CARTESIAN_POINT ( 'NONE',  ( 0.000000000000000000, 0.000000000000000000, -21.50000000000000000 ) ) ;
#72620=ORIENTED_EDGE ( 'NONE', *, *, #48541, .F. ) ;
#72699=DIRECTION ( 'NONE',  ( 1.000000000000000000, 0.000000000000000000, 0.000000000000000000 ) ) ;
#72735=CARTESIAN_POINT ( 'NONE',  ( 0.000000000000000000, 0.000000000000000000, -25.03750572909317285 ) ) ;
#72776=FACE_OUTER_BOUND ( 'NONE', #67175, .T. ) ;
#72800=DIRECTION ( 'NONE',  ( 0.000000000000000000, 0.000000000000000000, 1.000000000000000000 ) ) ;
#72810=STYLED_ITEM('',(#74706),#65418);
#72899=ORIENTED_EDGE ( 'NONE', *, *, #20387, .F. ) ;
#73049=CARTESIAN_POINT ( 'NONE',  ( 12.80255146922220888, 13.39305315375704097, -0.2939692054342086247 ) ) ;
#73084=DIRECTION ( 'NONE',  ( 0.000000000000000000, 0.000000000000000000, -1.000000000000000000 ) ) ;
#73098=ORIENTED_EDGE ( 'NONE', *, *, #51610, .T. ) ;
#73108=B_SPLINE_CURVE_WITH_KNOTS ( 'NONE', 3,
 ( #39466, #10791, #33453, #56453, #4771, #51152, #73049, #56086, #27763, #50775 ),
 .UNSPECIFIED., .F., .F.,
 ( 4, 2, 2, 2, 4 ),
 ( 0.01051554819734982701, 0.01182504667393347204, 0.01313454515051711881, 0.01575354210368441407, 0.02099153601001900113 ),
 .UNSPECIFIED. ) ;
#73257=EDGE_LOOP ( 'NONE', ( #48988, #31844, #39423, #53471, #42805, #9660 ) ) ;
#73411=CARTESIAN_POINT ( 'NONE',  ( -18.00000000000000355, -9.547192751170715752, -1.363732307033565183 ) ) ;
#73428=CARTESIAN_POINT ( 'NONE',  ( 15.04468117448323916, -12.09855896486656945, -0.7126204852947470858 ) ) ;
#73482=ADVANCED_FACE ( 'NONE', ( #28938 ), #23565, .T. ) ;
#73671=CARTESIAN_POINT ( 'NONE',  ( 0.000000000000000000, 0.000000000000000000, -20.42428869268542968 ) ) ;
#73678=CARTESIAN_POINT ( 'NONE',  ( 0.000000000000000000, 0.000000000000000000, -21.47459999999999525 ) ) ;
#73768=VECTOR ( 'NONE', #59893, 1000.000000000000000 ) ;
#74091=AXIS2_PLACEMENT_3D ( 'NONE', #36492, #13455, #14195 ) ;
#74189=DIRECTION ( 'NONE',  ( -0.8660254037844380415, -0.5000000000000012212, 0.000000000000000000 ) ) ;
#74280=DIRECTION ( 'NONE',  ( -1.000000000000000000, 0.000000000000000000, 0.000000000000000000 ) ) ;
#74544=EDGE_CURVE ( 'NONE', #71897, #70823, #37213, .T. ) ;
#74566=ORIENTED_EDGE ( 'NONE', *, *, #59046, .F. ) ;
#74604=CARTESIAN_POINT ( 'NONE',  ( -7.466667385518938715, -16.47372726584782043, -1.986122854721883435E-14 ) ) ;
#74700=COLOUR_RGB('Black',0.12,0.14,0.17);
#74701=FILL_AREA_STYLE_COLOUR('',#74700);
#74702=FILL_AREA_STYLE('',(#74701));
#74703=SURFACE_STYLE_FILL_AREA(#74702);
#74704=SURFACE_SIDE_STYLE('',(#74703));
#74705=SURFACE_STYLE_USAGE(.BOTH.,#74704);
#74706=PRESENTATION_STYLE_ASSIGNMENT((#74705));
ENDSEC;
END-ISO-10303-21;
